ISO-10303-21;
HEADER;
FILE_DESCRIPTION (('STEP AP214'),
    '1' );
FILE_NAME ('taper roller bearing_iso_ISO 355-2 - 2BD25 - 22,SI,NC,22.step',
    '2026-10-08T09:53:37',
    ( '' ),
    ( '' ),
    'SwSTEP 2.0',
    'SolidWorks 2026',
    '' );
FILE_SCHEMA (( 'AUTOMOTIVE_DESIGN' ));
ENDSEC;

DATA;
#98=TOROIDAL_SURFACE ( 'NONE', #51668, 20.69999999999999929, 0.2999999999999981570 ) ;
#123=DIRECTION ( 'NONE',  ( 0.000000000000000000, 0.000000000000000000, -1.000000000000000000 ) ) ;
#236=DIRECTION ( 'NONE',  ( 0.000000000000000000, 0.000000000000000000, -1.000000000000000000 ) ) ;
#240=ORIENTED_EDGE ( 'NONE', *, *, #37205, .F. ) ;
#287=CARTESIAN_POINT ( 'NONE',  ( -3.759344165985237129, 2.343521743652961183E-15, 19.05560546998412974 ) ) ;
#317=ADVANCED_FACE ( 'NONE', ( #65897 ), #60865, .T. ) ;
#671=CIRCLE ( 'NONE', #61866, 19.05560546998412974 ) ;
#709=DIRECTION ( 'NONE',  ( 0.000000000000000000, 0.000000000000000000, -1.000000000000000000 ) ) ;
#782=DIRECTION ( 'NONE',  ( 0.000000000000000000, 0.000000000000000000, 1.000000000000000000 ) ) ;
#810=EDGE_LOOP ( 'NONE', ( #25878, #42076, #22977, #8689 ) ) ;
#887=PRODUCT_CONTEXT ( 'NONE', #64237, 'mechanical' ) ;
#965=CIRCLE ( 'NONE', #50170, 0.2999999999999981570 ) ;
#966=CARTESIAN_POINT ( 'NONE',  ( 6.938893903907228378E-15, 0.000000000000000000, 0.000000000000000000 ) ) ;
#1073=EDGE_LOOP ( 'NONE', ( #38003, #2560, #56508, #46336 ) ) ;
#1146=ORIENTED_EDGE ( 'NONE', *, *, #73833, .F. ) ;
#1155=AXIS2_PLACEMENT_3D ( 'NONE', #13195, #24128, #69961 ) ;
#1259=ORIENTED_EDGE ( 'NONE', *, *, #39645, .F. ) ;
#1276=CONICAL_SURFACE ( 'NONE', #8416, 15.39727592608509177, 1.361356816555577609 ) ;
#1358=CARTESIAN_POINT ( 'NONE',  ( -10.90473778262209414, 0.000000000000000000, 0.000000000000000000 ) ) ;
#1448=ORIENTED_EDGE ( 'NONE', *, *, #18311, .T. ) ;
#1455=DIRECTION ( 'NONE',  ( 1.000000000000000000, 0.000000000000000000, 0.000000000000000000 ) ) ;
#1458=FACE_OUTER_BOUND ( 'NONE', #20264, .T. ) ;
#1580=DIRECTION ( 'NONE',  ( -0.7071067811865474617, 0.000000000000000000, 0.7071067811865474617 ) ) ;
#1616=( NAMED_UNIT ( * ) PLANE_ANGLE_UNIT ( ) SI_UNIT ( $, .RADIAN. ) );
#1626=CIRCLE ( 'NONE', #21979, 13.71399988598171049 ) ;
#1661=CARTESIAN_POINT ( 'NONE',  ( -11.99999999999999645, 2.553388576222231231E-15, 20.69999999999999929 ) ) ;
#1750=EDGE_CURVE ( 'NONE', #21370, #55509, #60500, .T. ) ;
#1903=CIRCLE ( 'NONE', #18644, 15.39727592589476579 ) ;
#2095=ORIENTED_EDGE ( 'NONE', *, *, #69495, .F. ) ;
#2252=ORIENTED_EDGE ( 'NONE', *, *, #13400, .F. ) ;
#2313=VECTOR ( 'NONE', #1580, 1000.000000000000114 ) ;
#2489=EDGE_LOOP ( 'NONE', ( #3517, #34755, #4345, #25455 ) ) ;
#2560=ORIENTED_EDGE ( 'NONE', *, *, #1750, .T. ) ;
#2685=STYLED_ITEM ( 'NONE', ( #59897 ), #3205 ) ;
#2922=DIRECTION ( 'NONE',  ( 0.000000000000000000, 0.000000000000000000, 1.000000000000000000 ) ) ;
#3032=EDGE_CURVE ( 'NONE', #61574, #61214, #73981, .T. ) ;
#3055=CARTESIAN_POINT ( 'NONE',  ( -42.50000000000000000, 0.000000000000000000, -20.99999999999999645 ) ) ;
#3081=SURFACE_SIDE_STYLE ('',( #47438 ) ) ;
#3107=DIRECTION ( 'NONE',  ( 0.000000000000000000, 0.000000000000000000, -1.000000000000000000 ) ) ;
#3137=( NAMED_UNIT ( * ) PLANE_ANGLE_UNIT ( ) SI_UNIT ( $, .RADIAN. ) );
#3154=ADVANCED_FACE ( 'NONE', ( #41624 ), #45400, .T. ) ;
#3205=ADVANCED_BREP_SHAPE_REPRESENTATION ( '', ( #14123, #43395 ), #57869 ) ;
#3279=DIRECTION ( 'NONE',  ( 1.000000000000000000, 0.000000000000000000, 0.000000000000000000 ) ) ;
#3375=ORIENTED_EDGE ( 'NONE', *, *, #36266, .T. ) ;
#3451=VERTEX_POINT ( 'NONE', #74271 ) ;
#3469=DIRECTION ( 'NONE',  ( 0.000000000000000000, 0.000000000000000000, -1.000000000000000000 ) ) ;
#3486=DIRECTION ( 'NONE',  ( 0.000000000000000000, 0.000000000000000000, -1.000000000000000000 ) ) ;
#3498=AXIS2_PLACEMENT_3D ( 'NONE', #61744, #27517, #38059 ) ;
#3517=ORIENTED_EDGE ( 'NONE', *, *, #14277, .F. ) ;
#3543=VERTEX_POINT ( 'NONE', #40813 ) ;
#3569=CARTESIAN_POINT ( 'NONE',  ( -2.977765906491215642, 0.000000000000000000, 0.000000000000000000 ) ) ;
#3897=LINE ( 'NONE', #26799, #73147 ) ;
#3939=ORIENTED_EDGE ( 'NONE', *, *, #73833, .T. ) ;
#3966=CARTESIAN_POINT ( 'NONE',  ( -3.759344165985237129, 0.000000000000000000, -19.05560546998412974 ) ) ;
#4007=ORIENTED_EDGE ( 'NONE', *, *, #55576, .F. ) ;
#4027=CONICAL_SURFACE ( 'NONE', #46037, 13.71319123027096865, 1.361356816555593596 ) ;
#4248=CONICAL_SURFACE ( 'NONE', #34229, 17.45460580326810174, 1.361356816555583826 ) ;
#4345=ORIENTED_EDGE ( 'NONE', *, *, #14696, .T. ) ;
#4356=CARTESIAN_POINT ( 'NONE',  ( -11.99999999999999645, 1.574895783703496238E-15, -12.85999999999999943 ) ) ;
#4387=DIRECTION ( 'NONE',  ( 0.000000000000000000, 0.000000000000000000, -1.000000000000000000 ) ) ;
#4397=PRODUCT_DEFINITION_SHAPE ( 'NONE', 'NONE',  #37077 ) ;
#4454=EDGE_LOOP ( 'NONE', ( #26529, #56816, #23611, #27016 ) ) ;
#4458=AXIS2_PLACEMENT_3D ( 'NONE', #14119, #43096, #25784 ) ;
#4548=AXIS2_PLACEMENT_3D ( 'NONE', #59057, #13182, #12803 ) ;
#4620=UNCERTAINTY_MEASURE_WITH_UNIT (LENGTH_MEASURE( 1.000000000000000082E-05 ), #71885, 'distance_accuracy_value', 'NONE');
#4622=AXIS2_PLACEMENT_3D ( 'NONE', #11804, #47155, #52405 ) ;
#4708=AXIS2_PLACEMENT_3D ( 'NONE', #50936, #23482, #46794 ) ;
#4740=DIRECTION ( 'NONE',  ( 1.000000000000000000, 0.000000000000000000, 0.000000000000000000 ) ) ;
#4759=AXIS2_PLACEMENT_3D ( 'NONE', #47824, #43324, #3107 ) ;
#4871=CARTESIAN_POINT ( 'NONE',  ( -2.977765906491215642, 1.885622467823562354E-15, 15.39727592589476579 ) ) ;
#4912=ORIENTED_EDGE ( 'NONE', *, *, #39645, .T. ) ;
#4925=DIRECTION ( 'NONE',  ( 0.000000000000000000, 0.000000000000000000, -1.000000000000000000 ) ) ;
#5018=FACE_BOUND ( 'NONE', #34003, .T. ) ;
#5024=ORIENTED_EDGE ( 'NONE', *, *, #6649, .F. ) ;
#5028=CARTESIAN_POINT ( 'NONE',  ( -12.00000000000000000, 0.000000000000000000, -17.30399999999999849 ) ) ;
#5062=DIRECTION ( 'NONE',  ( 1.000000000000000000, 0.000000000000000000, 0.000000000000000000 ) ) ;
#5097=ORIENTED_EDGE ( 'NONE', *, *, #65471, .T. ) ;
#5294=EDGE_CURVE ( 'NONE', #65590, #20976, #67934, .T. ) ;
#5352=EDGE_LOOP ( 'NONE', ( #50749, #72211, #49808, #25522 ) ) ;
#5363=CARTESIAN_POINT ( 'NONE',  ( -42.50000000000000000, 0.000000000000000000, 0.000000000000000000 ) ) ;
#5364=ORIENTED_EDGE ( 'NONE', *, *, #70095, .T. ) ;
#5376=ORIENTED_EDGE ( 'NONE', *, *, #5294, .T. ) ;
#5474=EDGE_CURVE ( 'NONE', #23517, #26896, #54774, .T. ) ;
#5475=VERTEX_POINT ( 'NONE', #72243 ) ;
#5489=CARTESIAN_POINT ( 'NONE',  ( -42.50000000000000000, 0.000000000000000000, 0.000000000000000000 ) ) ;
#5507=DIRECTION ( 'NONE',  ( 1.000000000000000000, 0.000000000000000000, 0.000000000000000000 ) ) ;
#5508=DIRECTION ( 'NONE',  ( 0.000000000000000000, 0.000000000000000000, 1.000000000000000000 ) ) ;
#5730=VECTOR ( 'NONE', #65164, 1000.000000000000227 ) ;
#5731=FACE_OUTER_BOUND ( 'NONE', #45906, .T. ) ;
#5761=SHAPE_DEFINITION_REPRESENTATION ( #4397, #42128 ) ;
#5838=DIRECTION ( 'NONE',  ( -1.000000000000000000, 0.000000000000000000, 0.000000000000000000 ) ) ;
#5854=DIRECTION ( 'NONE',  ( 0.000000000000000000, 0.000000000000000000, -1.000000000000000000 ) ) ;
#5908=DIRECTION ( 'NONE',  ( 1.000000000000000000, 0.000000000000000000, 0.000000000000000000 ) ) ;
#6118=VECTOR ( 'NONE', #45449, 1000.000000000000114 ) ;
#6257=( GEOMETRIC_REPRESENTATION_CONTEXT ( 3 ) GLOBAL_UNCERTAINTY_ASSIGNED_CONTEXT ( ( #21885 ) ) GLOBAL_UNIT_ASSIGNED_CONTEXT ( ( #65167, #25668, #59016 ) ) REPRESENTATION_CONTEXT ( 'NONE', 'WORKASPACE' ) );
#6412=ORIENTED_EDGE ( 'NONE', *, *, #5474, .T. ) ;
#6638=AXIS2_PLACEMENT_3D ( 'NONE', #32924, #55874, #4387 ) ;
#6649=EDGE_CURVE ( 'NONE', #24509, #58812, #13627, .T. ) ;
#7051=CONICAL_SURFACE ( 'NONE', #13055, 17.30399999999999849, 0.2094395102393129815 ) ;
#7099=AXIS2_PLACEMENT_3D ( 'NONE', #64251, #36030, #51848 ) ;
#7228=AXIS2_PLACEMENT_3D ( 'NONE', #55026, #43766, #66686 ) ;
#7262=DIRECTION ( 'NONE',  ( 1.000000000000000000, 0.000000000000000000, 0.000000000000000000 ) ) ;
#7348=VERTEX_POINT ( 'NONE', #4871 ) ;
#7378=EDGE_CURVE ( 'NONE', #61574, #5475, #43702, .T. ) ;
#7393=DIRECTION ( 'NONE',  ( 1.000000000000000000, 0.000000000000000000, 0.000000000000000000 ) ) ;
#7466=CARTESIAN_POINT ( 'NONE',  ( 3.469446951953614189E-15, 12.79999999999999893, 0.000000000000000000 ) ) ;
#7520=DIRECTION ( 'NONE',  ( 1.000000000000000000, -0.000000000000000000, -0.000000000000000000 ) ) ;
#7522=EDGE_LOOP ( 'NONE', ( #7619, #37907 ) ) ;
#7565=ORIENTED_EDGE ( 'NONE', *, *, #35091, .T. ) ;
#7583=FILL_AREA_STYLE ('',( #31607 ) ) ;
#7609=CARTESIAN_POINT ( 'NONE',  ( -12.00000000000000000, 0.000000000000000000, 0.000000000000000000 ) ) ;
#7619=ORIENTED_EDGE ( 'NONE', *, *, #20014, .F. ) ;
#7670=AXIS2_PLACEMENT_3D ( 'NONE', #56735, #28499, #22134 ) ;
#7675=ORIENTED_EDGE ( 'NONE', *, *, #18570, .T. ) ;
#7769=EDGE_LOOP ( 'NONE', ( #58424, #55135, #31790, #7675 ) ) ;
#7832=DIRECTION ( 'NONE',  ( 0.000000000000000000, 0.000000000000000000, -1.000000000000000000 ) ) ;
#7989=CARTESIAN_POINT ( 'NONE',  ( -11.70000000000000107, 2.137572712735109784E-15, -17.45460580326810174 ) ) ;
#8014=COLOUR_RGB ( '', 0.08235294, 0.09019608, 0.10196078) ;
#8151=CARTESIAN_POINT ( 'NONE',  ( -3.360000000000002096, 0.000000000000000000, 0.000000000000000000 ) ) ;
#8181=DIRECTION ( 'NONE',  ( 0.9781476007338070211, 2.546183866652749098E-17, 0.2079116908177526257 ) ) ;
#8239=ORIENTED_EDGE ( 'NONE', *, *, #11386, .T. ) ;
#8301=ADVANCED_FACE ( 'NONE', ( #67824, #11057 ), #56559, .T. ) ;
#8351=CARTESIAN_POINT ( 'NONE',  ( -11.99999999999999645, 0.000000000000000000, 0.000000000000000000 ) ) ;
#8362=AXIS2_PLACEMENT_3D ( 'NONE', #23872, #63737, #5854 ) ;
#8369=DIRECTION ( 'NONE',  ( 0.000000000000000000, 0.000000000000000000, -1.000000000000000000 ) ) ;
#8416=AXIS2_PLACEMENT_3D ( 'NONE', #10988, #45587, #62886 ) ;
#8468=VECTOR ( 'NONE', #48920, 1000.000000000000114 ) ;
#8602=CONICAL_SURFACE ( 'NONE', #30218, 13.71319123027096865, 1.361356816555593596 ) ;
#8689=ORIENTED_EDGE ( 'NONE', *, *, #45338, .F. ) ;
#8727=DIRECTION ( 'NONE',  ( 0.000000000000000000, 0.000000000000000000, -1.000000000000000000 ) ) ;
#8835=VECTOR ( 'NONE', #73728, 1000.000000000000114 ) ;
#8944=ORIENTED_EDGE ( 'NONE', *, *, #19014, .F. ) ;
#9021=DIRECTION ( 'NONE',  ( -0.2079116908177527367, 0.000000000000000000, 0.9781476007338070211 ) ) ;
#9114=SURFACE_STYLE_USAGE ( .BOTH. , #37702 ) ;
#9163=FACE_OUTER_BOUND ( 'NONE', #810, .T. ) ;
#9234=CIRCLE ( 'NONE', #38062, 20.99999999999999645 ) ;
#9484=DIRECTION ( 'NONE',  ( 1.000000000000000000, 0.000000000000000000, 0.000000000000000000 ) ) ;
#9723=CIRCLE ( 'NONE', #57769, 17.30399999999999849 ) ;
#9759=CARTESIAN_POINT ( 'NONE',  ( -10.90076147243505211, 0.000000000000000000, 13.71319123027096865 ) ) ;
#9868=DIRECTION ( 'NONE',  ( 0.000000000000000000, 0.000000000000000000, -1.000000000000000000 ) ) ;
#9874=ORIENTED_EDGE ( 'NONE', *, *, #39727, .F. ) ;
#9959=CARTESIAN_POINT ( 'NONE',  ( -10.90076147243505211, 1.679381574624689562E-15, -13.71319123027096865 ) ) ;
#10124=DIRECTION ( 'NONE',  ( 1.000000000000000000, 0.000000000000000000, 0.000000000000000000 ) ) ;
#10351=ORIENTED_EDGE ( 'NONE', *, *, #30279, .T. ) ;
#10426=ADVANCED_FACE ( 'NONE', ( #41003 ), #16731, .F. ) ;
#10465=ORIENTED_EDGE ( 'NONE', *, *, #20489, .F. ) ;
#10471=CARTESIAN_POINT ( 'NONE',  ( -3.000000000000002665, 0.000000000000000000, 20.64000000000000057 ) ) ;
#10584=VECTOR ( 'NONE', #65156, 1000.000000000000000 ) ;
#10722=DIRECTION ( 'NONE',  ( 0.9781476007338069101, 2.546183866652752180E-17, 0.2079116908177528755 ) ) ;
#10935=AXIS2_PLACEMENT_3D ( 'NONE', #28163, #11600, #11247 ) ;
#10988=CARTESIAN_POINT ( 'NONE',  ( -2.981742216678212820, 0.000000000000000000, 0.000000000000000000 ) ) ;
#11043=ADVANCED_FACE ( 'NONE', ( #31824 ), #28799, .T. ) ;
#11057=FACE_BOUND ( 'NONE', #29187, .T. ) ;
#11141=CIRCLE ( 'NONE', #21970, 17.30399999999999849 ) ;
#11149=CIRCLE ( 'NONE', #17102, 15.39727592608509177 ) ;
#11187=DIRECTION ( 'NONE',  ( 0.000000000000000000, 1.000000000000000000, -1.224646799147353207E-16 ) ) ;
#11247=DIRECTION ( 'NONE',  ( 0.000000000000000000, 0.000000000000000000, 1.000000000000000000 ) ) ;
#11318=CARTESIAN_POINT ( 'NONE',  ( -2.981742216678212820, 0.000000000000000000, 0.000000000000000000 ) ) ;
#11386=EDGE_CURVE ( 'NONE', #35978, #3451, #25648, .T. ) ;
#11490=CARTESIAN_POINT ( 'NONE',  ( -12.00000000000000000, 0.000000000000000000, 0.000000000000000000 ) ) ;
#11587=CLOSED_SHELL ( 'NONE', ( #54893, #46543, #73347, #56205, #72733, #44152, #49656, #69832, #10426, #16377, #47424, #31562, #45234, #72280, #17641, #63496, #8301, #70527, #54217, #22752, #25823, #3154, #42387, #17499, #45374, #22535, #32315, #64955, #70601, #46203, #317, #44578, #29512, #60801, #11043 ) ) ;
#11600=DIRECTION ( 'NONE',  ( 1.000000000000000000, -0.000000000000000000, -0.000000000000000000 ) ) ;
#11769=ORIENTED_EDGE ( 'NONE', *, *, #19014, .T. ) ;
#11804=CARTESIAN_POINT ( 'NONE',  ( -42.50000000000000000, 0.000000000000000000, 0.000000000000000000 ) ) ;
#11891=CIRCLE ( 'NONE', #53932, 13.90444123027096879 ) ;
#11915=EDGE_LOOP ( 'NONE', ( #23061, #58936, #29942, #69887 ) ) ;
#12286=EDGE_LOOP ( 'NONE', ( #30026, #50422, #39105, #7565 ) ) ;
#12476=ORIENTED_EDGE ( 'NONE', *, *, #20489, .T. ) ;
#12512=ORIENTED_EDGE ( 'NONE', *, *, #5474, .F. ) ;
#12677=CARTESIAN_POINT ( 'NONE',  ( -11.99999999999999645, 0.000000000000000000, 0.000000000000000000 ) ) ;
#12721=FACE_BOUND ( 'NONE', #25764, .T. ) ;
#12803=DIRECTION ( 'NONE',  ( 0.000000000000000000, 0.000000000000000000, 1.000000000000000000 ) ) ;
#12858=CIRCLE ( 'NONE', #53660, 15.77977592589476608 ) ;
#13055=AXIS2_PLACEMENT_3D ( 'NONE', #17718, #70315, #40663 ) ;
#13097=AXIS2_PLACEMENT_3D ( 'NONE', #58182, #64206, #35611 ) ;
#13146=CARTESIAN_POINT ( 'NONE',  ( -10.90473778262209414, 0.000000000000000000, 0.000000000000000000 ) ) ;
#13181=CARTESIAN_POINT ( 'NONE',  ( -11.70000000000000107, 0.000000000000000000, 17.45460580326810174 ) ) ;
#13182=DIRECTION ( 'NONE',  ( -1.000000000000000000, 0.000000000000000000, 0.000000000000000000 ) ) ;
#13195=CARTESIAN_POINT ( 'NONE',  ( -2.977765906491215642, 0.000000000000000000, 0.000000000000000000 ) ) ;
#13253=DIRECTION ( 'NONE',  ( 1.000000000000000000, 0.000000000000000000, 0.000000000000000000 ) ) ;
#13307=CARTESIAN_POINT ( 'NONE',  ( -0.2999999999999964362, 1.567547902908612184E-15, 12.80000000000000071 ) ) ;
#13390=CARTESIAN_POINT ( 'NONE',  ( -42.50000000000000000, 2.571758278209441267E-15, 20.99999999999999645 ) ) ;
#13400=EDGE_CURVE ( 'NONE', #73994, #26896, #21994, .T. ) ;
#13414=EDGE_CURVE ( 'NONE', #69389, #66054, #31073, .T. ) ;
#13475=EDGE_CURVE ( 'NONE', #35978, #32156, #21464, .T. ) ;
#13627=CIRCLE ( 'NONE', #64045, 12.85999999999999943 ) ;
#13629=DIRECTION ( 'NONE',  ( 1.000000000000000000, 0.000000000000000000, 0.000000000000000000 ) ) ;
#13888=EDGE_CURVE ( 'NONE', #66054, #35854, #3897, .T. ) ;
#13920=EDGE_CURVE ( 'NONE', #38741, #56010, #9234, .T. ) ;
#13971=DIRECTION ( 'NONE',  ( 1.000000000000000000, 0.000000000000000000, 0.000000000000000000 ) ) ;
#13997=AXIS2_PLACEMENT_3D ( 'NONE', #37691, #49682, #3486 ) ;
#14119=CARTESIAN_POINT ( 'NONE',  ( -11.99999999999999645, 0.000000000000000000, 0.000000000000000000 ) ) ;
#14123=MANIFOLD_SOLID_BREP ( 'InnerRace', #11587 ) ;
#14131=CIRCLE ( 'NONE', #23752, 20.69999999999999929 ) ;
#14277=EDGE_CURVE ( 'NONE', #5475, #61574, #54907, .T. ) ;
#14285=AXIS2_PLACEMENT_3D ( 'NONE', #47160, #5838, #70427 ) ;
#14289=LINE ( 'NONE', #13181, #20294 ) ;
#14355=FACE_OUTER_BOUND ( 'NONE', #73810, .T. ) ;
#14621=VECTOR ( 'NONE', #13253, 1000.000000000000000 ) ;
#14662=VECTOR ( 'NONE', #69017, 1000.000000000000114 ) ;
#14696=EDGE_CURVE ( 'NONE', #20114, #61214, #44080, .T. ) ;
#14712=FACE_OUTER_BOUND ( 'NONE', #7522, .T. ) ;
#14748=FILL_AREA_STYLE ('',( #36950 ) ) ;
#14822=ORIENTED_EDGE ( 'NONE', *, *, #13400, .T. ) ;
#15186=EDGE_CURVE ( 'NONE', #19812, #67617, #11141, .T. ) ;
#15597=ORIENTED_EDGE ( 'NONE', *, *, #71050, .F. ) ;
#15628=DIRECTION ( 'NONE',  ( -1.000000000000000000, 0.000000000000000000, 0.000000000000000000 ) ) ;
#15851=TOROIDAL_SURFACE ( 'NONE', #67475, 20.69999999999999929, 0.2999999999999981570 ) ;
#15905=PLANE ( 'NONE',  #50091 ) ;
#16147=DIRECTION ( 'NONE',  ( 0.9781476007338069101, 2.546183866652752180E-17, 0.2079116908177528755 ) ) ;
#16236=DIRECTION ( 'NONE',  ( 1.000000000000000000, 0.000000000000000000, 0.000000000000000000 ) ) ;
#16377=ADVANCED_FACE ( 'NONE', ( #46604 ), #37704, .F. ) ;
#16488=LINE ( 'NONE', #55967, #6118 ) ;
#16694=CARTESIAN_POINT ( 'NONE',  ( -3.000000000000000888, 20.64000000000000057, 0.000000000000000000 ) ) ;
#16731=CONICAL_SURFACE ( 'NONE', #41956, 13.71319123046128752, 0.2094395102393127317 ) ;
#16833=VERTEX_POINT ( 'NONE', #22479 ) ;
#17102=AXIS2_PLACEMENT_3D ( 'NONE', #11318, #17333, #57934 ) ;
#17333=DIRECTION ( 'NONE',  ( 1.000000000000000000, -0.000000000000000000, -0.000000000000000000 ) ) ;
#17363=DIRECTION ( 'NONE',  ( 1.000000000000000000, 0.000000000000000000, 0.000000000000000000 ) ) ;
#17499=ADVANCED_FACE ( 'NONE', ( #64841 ), #42268, .F. ) ;
#17517=CIRCLE ( 'NONE', #59542, 12.50000000000000000 ) ;
#17641=ADVANCED_FACE ( 'NONE', ( #66683 ), #54515, .F. ) ;
#17645=CIRCLE ( 'NONE', #4458, 20.69999999999999929 ) ;
#17671=AXIS2_PLACEMENT_3D ( 'NONE', #26263, #73613, #67990 ) ;
#17718=CARTESIAN_POINT ( 'NONE',  ( -12.00000000000000000, 0.000000000000000000, 0.000000000000000000 ) ) ;
#17750=AXIS2_PLACEMENT_3D ( 'NONE', #69957, #47411, #52308 ) ;
#17782=EDGE_LOOP ( 'NONE', ( #49937, #42938, #40239, #10465 ) ) ;
#17930=CIRCLE ( 'NONE', #4759, 15.77977592589476608 ) ;
#17956=DIRECTION ( 'NONE',  ( 1.000000000000000000, 0.000000000000000000, 0.000000000000000000 ) ) ;
#17981=ORIENTED_EDGE ( 'NONE', *, *, #24948, .T. ) ;
#18084=DIRECTION ( 'NONE',  ( 0.000000000000000000, 0.000000000000000000, 1.000000000000000000 ) ) ;
#18139=CARTESIAN_POINT ( 'NONE',  ( -11.99999999999999645, 0.000000000000000000, -20.69999999999999929 ) ) ;
#18289=ORIENTED_EDGE ( 'NONE', *, *, #28436, .F. ) ;
#18311=EDGE_CURVE ( 'NONE', #38823, #18520, #54560, .T. ) ;
#18348=FACE_OUTER_BOUND ( 'NONE', #2489, .T. ) ;
#18365=FACE_OUTER_BOUND ( 'NONE', #66509, .T. ) ;
#18404=SHAPE_REPRESENTATION_RELATIONSHIP ( 'NONE' , 'NONE' ,  #42128, #3205 ) ;
#18441=FACE_OUTER_BOUND ( 'NONE', #29493, .T. ) ;
#18442=EDGE_CURVE ( 'NONE', #35854, #73994, #671, .T. ) ;
#18455=DIRECTION ( 'NONE',  ( -1.000000000000000000, -0.000000000000000000, -0.000000000000000000 ) ) ;
#18463=ORIENTED_EDGE ( 'NONE', *, *, #30279, .F. ) ;
#18520=VERTEX_POINT ( 'NONE', #54761 ) ;
#18524=CARTESIAN_POINT ( 'NONE',  ( -3.000000000000002665, 0.000000000000000000, 0.000000000000000000 ) ) ;
#18536=CIRCLE ( 'NONE', #60568, 0.2999999999999981570 ) ;
#18570=EDGE_CURVE ( 'NONE', #18520, #38823, #63070, .T. ) ;
#18644=AXIS2_PLACEMENT_3D ( 'NONE', #3569, #20829, #20468 ) ;
#18684=DIRECTION ( 'NONE',  ( 0.000000000000000000, 0.000000000000000000, -1.000000000000000000 ) ) ;
#18878=CARTESIAN_POINT ( 'NONE',  ( -0.2999999999999947153, 0.000000000000000000, 0.000000000000000000 ) ) ;
#18897=AXIS2_PLACEMENT_3D ( 'NONE', #74068, #38386, #67700 ) ;
#18911=LINE ( 'NONE', #41856, #49452 ) ;
#19014=EDGE_CURVE ( 'NONE', #7348, #54917, #1903, .T. ) ;
#19015=ORIENTED_EDGE ( 'NONE', *, *, #37536, .T. ) ;
#19093=CARTESIAN_POINT ( 'NONE',  ( -10.90473778262209414, 1.679381574647996852E-15, 13.71319123046128752 ) ) ;
#19200=DIRECTION ( 'NONE',  ( -1.000000000000000000, 0.000000000000000000, 0.000000000000000000 ) ) ;
#19283=SURFACE_STYLE_FILL_AREA ( #14748 ) ;
#19305=EDGE_LOOP ( 'NONE', ( #4007, #50692, #61021, #39234 ) ) ;
#19342=CARTESIAN_POINT ( 'NONE',  ( -3.000000000000002665, 2.549714635824789697E-15, -20.64000000000000057 ) ) ;
#19374=EDGE_CURVE ( 'NONE', #5475, #20114, #57144, .T. ) ;
#19391=CIRCLE ( 'NONE', #70965, 15.77977592589476608 ) ;
#19399=CARTESIAN_POINT ( 'NONE',  ( -3.360000000000002096, 0.000000000000000000, -21.00000000000000000 ) ) ;
#19605=CARTESIAN_POINT ( 'NONE',  ( -0.2999999999999947153, 1.530808498934191521E-15, 12.50000000000000000 ) ) ;
#19735=DIRECTION ( 'NONE',  ( 1.000000000000000000, 0.000000000000000000, 0.000000000000000000 ) ) ;
#19812=VERTEX_POINT ( 'NONE', #5028 ) ;
#19956=SURFACE_STYLE_USAGE ( .BOTH. , #3081 ) ;
#19987=FACE_BOUND ( 'NONE', #24950, .T. ) ;
#20014=EDGE_CURVE ( 'NONE', #58552, #68894, #30456, .T. ) ;
#20114=VERTEX_POINT ( 'NONE', #19605 ) ;
#20148=AXIS2_PLACEMENT_3D ( 'NONE', #63836, #35248, #58179 ) ;
#20158=DIRECTION ( 'NONE',  ( 0.000000000000000000, 0.000000000000000000, -1.000000000000000000 ) ) ;
#20161=CIRCLE ( 'NONE', #17750, 19.21700905503013601 ) ;
#20179=ORIENTED_EDGE ( 'NONE', *, *, #49642, .T. ) ;
#20196=CYLINDRICAL_SURFACE ( 'NONE', #29787, 15.77977592589476608 ) ;
#20264=EDGE_LOOP ( 'NONE', ( #39956, #14822, #25955, #60799 ) ) ;
#20294=VECTOR ( 'NONE', #9021, 1000.000000000000000 ) ;
#20298=CARTESIAN_POINT ( 'NONE',  ( -3.000000000000002665, 0.000000000000000000, 20.64000000000000057 ) ) ;
#20307=LINE ( 'NONE', #3055, #68300 ) ;
#20344=CONICAL_SURFACE ( 'NONE', #51581, 12.85999999999999943, 0.7853981633974482790 ) ;
#20454=EDGE_CURVE ( 'NONE', #68894, #58552, #33824, .T. ) ;
#20468=DIRECTION ( 'NONE',  ( 0.000000000000000000, 0.000000000000000000, -1.000000000000000000 ) ) ;
#20489=EDGE_CURVE ( 'NONE', #41023, #61214, #21802, .T. ) ;
#20583=CARTESIAN_POINT ( 'NONE',  ( -11.99999999999999645, 0.000000000000000000, 0.000000000000000000 ) ) ;
#20812=DIRECTION ( 'NONE',  ( 1.000000000000000000, 0.000000000000000000, 0.000000000000000000 ) ) ;
#20829=DIRECTION ( 'NONE',  ( 1.000000000000000000, 0.000000000000000000, 0.000000000000000000 ) ) ;
#20877=EDGE_CURVE ( 'NONE', #61574, #24509, #35163, .T. ) ;
#20888=EDGE_LOOP ( 'NONE', ( #41636, #44612, #10351, #67715 ) ) ;
#20976=VERTEX_POINT ( 'NONE', #19342 ) ;
#21081=FACE_BOUND ( 'NONE', #70491, .T. ) ;
#21246=ORIENTED_EDGE ( 'NONE', *, *, #3032, .T. ) ;
#21268=CARTESIAN_POINT ( 'NONE',  ( -3.759344165985237129, 0.000000000000000000, 0.000000000000000000 ) ) ;
#21337=ORIENTED_EDGE ( 'NONE', *, *, #1750, .F. ) ;
#21370=VERTEX_POINT ( 'NONE', #60521 ) ;
#21380=CARTESIAN_POINT ( 'NONE',  ( -10.90093335751250692, 0.000000000000000000, 0.000000000000000000 ) ) ;
#21464=CIRCLE ( 'NONE', #14285, 13.90444123027096879 ) ;
#21758=ORIENTED_EDGE ( 'NONE', *, *, #43886, .F. ) ;
#21770=FACE_OUTER_BOUND ( 'NONE', #37210, .T. ) ;
#21802=CIRCLE ( 'NONE', #65025, 0.2999999999999999334 ) ;
#21885=UNCERTAINTY_MEASURE_WITH_UNIT (LENGTH_MEASURE( 1.000000000000000082E-05 ), #65167, 'distance_accuracy_value', 'NONE');
#21906=DIRECTION ( 'NONE',  ( -0.2079116908177587875, 1.197885328332318196E-16, -0.9781476007338056888 ) ) ;
#21970=AXIS2_PLACEMENT_3D ( 'NONE', #11490, #5507, #28405 ) ;
#21979=AXIS2_PLACEMENT_3D ( 'NONE', #21380, #27399, #28515 ) ;
#21994=LINE ( 'NONE', #27998, #68339 ) ;
#22134=DIRECTION ( 'NONE',  ( 0.000000000000000000, 0.000000000000000000, -1.000000000000000000 ) ) ;
#22149=DIRECTION ( 'NONE',  ( 0.000000000000000000, 0.000000000000000000, 1.000000000000000000 ) ) ;
#22181=CARTESIAN_POINT ( 'NONE',  ( -42.50000000000000000, 1.530808498934191521E-15, 12.50000000000000000 ) ) ;
#22444=CARTESIAN_POINT ( 'NONE',  ( -2.981742216678212820, 0.000000000000000000, 15.39727592608509177 ) ) ;
#22479=CARTESIAN_POINT ( 'NONE',  ( -11.68233973192911535, 2.127397731264211754E-15, 17.37152077436032371 ) ) ;
#22496=CARTESIAN_POINT ( 'NONE',  ( -42.50000000000000000, 0.000000000000000000, -12.50000000000000000 ) ) ;
#22535=ADVANCED_FACE ( 'NONE', ( #18441 ), #8602, .T. ) ;
#22752=ADVANCED_FACE ( 'NONE', ( #27791 ), #15851, .T. ) ;
#22905=DIRECTION ( 'NONE',  ( -1.000000000000000000, -0.000000000000000000, -0.000000000000000000 ) ) ;
#22934=ORIENTED_EDGE ( 'NONE', *, *, #36644, .F. ) ;
#22977=ORIENTED_EDGE ( 'NONE', *, *, #53907, .F. ) ;
#23028=ORIENTED_EDGE ( 'NONE', *, *, #15186, .T. ) ;
#23030=ORIENTED_EDGE ( 'NONE', *, *, #13475, .T. ) ;
#23045=MECHANICAL_DESIGN_GEOMETRIC_PRESENTATION_REPRESENTATION('',(#2685),#6257);
#23061=ORIENTED_EDGE ( 'NONE', *, *, #20014, .T. ) ;
#23482=DIRECTION ( 'NONE',  ( 1.000000000000000000, -0.000000000000000000, -0.000000000000000000 ) ) ;
#23517=VERTEX_POINT ( 'NONE', #53521 ) ;
#23545=AXIS2_PLACEMENT_3D ( 'NONE', #18524, #7262, #23805 ) ;
#23611=ORIENTED_EDGE ( 'NONE', *, *, #62214, .T. ) ;
#23752=AXIS2_PLACEMENT_3D ( 'NONE', #73496, #4740, #62621 ) ;
#23805=DIRECTION ( 'NONE',  ( 0.000000000000000000, 0.000000000000000000, -1.000000000000000000 ) ) ;
#23872=CARTESIAN_POINT ( 'NONE',  ( -42.50000000000000000, 0.000000000000000000, 0.000000000000000000 ) ) ;
#24008=DIRECTION ( 'NONE',  ( 1.000000000000000000, 0.000000000000000000, 0.000000000000000000 ) ) ;
#24078=CONICAL_SURFACE ( 'NONE', #13097, 17.30399999999999849, 0.2094395102393129815 ) ;
#24119=CARTESIAN_POINT ( 'NONE',  ( -42.50000000000000000, 0.000000000000000000, 0.000000000000000000 ) ) ;
#24128=DIRECTION ( 'NONE',  ( 1.000000000000000000, 0.000000000000000000, 0.000000000000000000 ) ) ;
#24149=DIRECTION ( 'NONE',  ( 0.000000000000000000, 0.000000000000000000, -1.000000000000000000 ) ) ;
#24284=EDGE_CURVE ( 'NONE', #68149, #3543, #64538, .T. ) ;
#24324=LINE ( 'NONE', #57427, #37045 ) ;
#24509=VERTEX_POINT ( 'NONE', #4356 ) ;
#24560=DIRECTION ( 'NONE',  ( 0.000000000000000000, 1.000000000000000000, -1.224646799147353207E-16 ) ) ;
#24584=ORIENTED_EDGE ( 'NONE', *, *, #65546, .T. ) ;
#24664=VERTEX_POINT ( 'NONE', #29750 ) ;
#24714=AXIS2_PLACEMENT_3D ( 'NONE', #5363, #51570, #123 ) ;
#24748=DIRECTION ( 'NONE',  ( 1.000000000000000000, 0.000000000000000000, 0.000000000000000000 ) ) ;
#24762=AXIS2_PLACEMENT_3D ( 'NONE', #43339, #66620, #8369 ) ;
#24941=EDGE_LOOP ( 'NONE', ( #2252, #62147, #5364, #6412 ) ) ;
#24948=EDGE_CURVE ( 'NONE', #58812, #24509, #73730, .T. ) ;
#24950=EDGE_LOOP ( 'NONE', ( #29085, #11769 ) ) ;
#25106=DIRECTION ( 'NONE',  ( 0.000000000000000000, 0.000000000000000000, -1.000000000000000000 ) ) ;
#25156=AXIS2_PLACEMENT_3D ( 'NONE', #13307, #11187, #34117 ) ;
#25223=CYLINDRICAL_SURFACE ( 'NONE', #41965, 13.90444123027096879 ) ;
#25280=PLANE ( 'NONE',  #49966 ) ;
#25379=CIRCLE ( 'NONE', #67380, 12.79999999999999893 ) ;
#25441=CARTESIAN_POINT ( 'NONE',  ( -2.977765906491215642, 0.000000000000000000, 0.000000000000000000 ) ) ;
#25455=ORIENTED_EDGE ( 'NONE', *, *, #3032, .F. ) ;
#25522=ORIENTED_EDGE ( 'NONE', *, *, #46939, .F. ) ;
#25648=LINE ( 'NONE', #7989, #37283 ) ;
#25660=PRODUCT_DEFINITION_FORMATION_WITH_SPECIFIED_SOURCE ( 'ANY', '', #37971, .NOT_KNOWN. ) ;
#25668=( NAMED_UNIT ( * ) PLANE_ANGLE_UNIT ( ) SI_UNIT ( $, .RADIAN. ) );
#25764=EDGE_LOOP ( 'NONE', ( #73745, #15597 ) ) ;
#25784=DIRECTION ( 'NONE',  ( 0.000000000000000000, 0.000000000000000000, -1.000000000000000000 ) ) ;
#25823=ADVANCED_FACE ( 'NONE', ( #68638 ), #34033, .T. ) ;
#25878=ORIENTED_EDGE ( 'NONE', *, *, #48063, .T. ) ;
#25955=ORIENTED_EDGE ( 'NONE', *, *, #36644, .T. ) ;
#26078=CARTESIAN_POINT ( 'NONE',  ( -12.00000000000000000, 0.000000000000000000, 0.000000000000000000 ) ) ;
#26263=CARTESIAN_POINT ( 'NONE',  ( -0.2999999999999947153, 0.000000000000000000, 0.000000000000000000 ) ) ;
#26322=CIRCLE ( 'NONE', #1155, 15.39727592589476579 ) ;
#26345=EDGE_LOOP ( 'NONE', ( #66226, #50681, #43439, #8944 ) ) ;
#26364=CARTESIAN_POINT ( 'NONE',  ( -11.99999999999999645, 0.000000000000000000, 12.85999999999999943 ) ) ;
#26369=VERTEX_POINT ( 'NONE', #18139 ) ;
#26529=ORIENTED_EDGE ( 'NONE', *, *, #50984, .F. ) ;
#26533=CIRCLE ( 'NONE', #63802, 17.37152077436032371 ) ;
#26625=ORIENTED_EDGE ( 'NONE', *, *, #37536, .F. ) ;
#26667=CARTESIAN_POINT ( 'NONE',  ( -11.70000000000000107, 0.000000000000000000, 0.000000000000000000 ) ) ;
#26799=CARTESIAN_POINT ( 'NONE',  ( -2.981742216678212820, 1.885622467846870828E-15, -15.39727592608509177 ) ) ;
#26805=FACE_OUTER_BOUND ( 'NONE', #42379, .T. ) ;
#26896=VERTEX_POINT ( 'NONE', #66747 ) ;
#27016=ORIENTED_EDGE ( 'NONE', *, *, #28207, .F. ) ;
#27068=EDGE_LOOP ( 'NONE', ( #44966, #53832, #63416, #2095 ) ) ;
#27130=ORIENTED_EDGE ( 'NONE', *, *, #55576, .T. ) ;
#27210=MECHANICAL_DESIGN_GEOMETRIC_PRESENTATION_REPRESENTATION('',(#65653),#70462);
#27399=DIRECTION ( 'NONE',  ( 1.000000000000000000, 0.000000000000000000, 0.000000000000000000 ) ) ;
#27401=FACE_OUTER_BOUND ( 'NONE', #17782, .T. ) ;
#27517=DIRECTION ( 'NONE',  ( 1.000000000000000000, 0.000000000000000000, 0.000000000000000000 ) ) ;
#27553=ORIENTED_EDGE ( 'NONE', *, *, #28207, .T. ) ;
#27791=FACE_OUTER_BOUND ( 'NONE', #4454, .T. ) ;
#27998=CARTESIAN_POINT ( 'NONE',  ( -12.00000000000000000, 2.119128821244579932E-15, 17.30399999999999849 ) ) ;
#28008=ORIENTED_EDGE ( 'NONE', *, *, #53907, .T. ) ;
#28098=AXIS2_PLACEMENT_3D ( 'NONE', #26078, #20812, #49006 ) ;
#28163=CARTESIAN_POINT ( 'NONE',  ( -3.759344165985237129, 0.000000000000000000, 0.000000000000000000 ) ) ;
#28207=EDGE_CURVE ( 'NONE', #56010, #38741, #45446, .T. ) ;
#28263=LINE ( 'NONE', #46679, #72054 ) ;
#28273=EDGE_CURVE ( 'NONE', #68894, #32156, #70022, .T. ) ;
#28405=DIRECTION ( 'NONE',  ( 0.000000000000000000, 0.000000000000000000, -1.000000000000000000 ) ) ;
#28436=EDGE_CURVE ( 'NONE', #41131, #54917, #53490, .T. ) ;
#28467=VERTEX_POINT ( 'NONE', #1661 ) ;
#28499=DIRECTION ( 'NONE',  ( 1.000000000000000000, 0.000000000000000000, 0.000000000000000000 ) ) ;
#28515=DIRECTION ( 'NONE',  ( 0.000000000000000000, 0.000000000000000000, 1.000000000000000000 ) ) ;
#28770=CARTESIAN_POINT ( 'NONE',  ( -2.977765906491215642, 0.000000000000000000, -15.39727592589476579 ) ) ;
#28781=CARTESIAN_POINT ( 'NONE',  ( -11.99999999999999645, 1.574895783703496238E-15, -12.85999999999999943 ) ) ;
#28799=CONICAL_SURFACE ( 'NONE', #49176, 15.39727592589476579, 0.2094395102393128150 ) ;
#28834=ORIENTED_EDGE ( 'NONE', *, *, #7378, .F. ) ;
#29085=ORIENTED_EDGE ( 'NONE', *, *, #45583, .T. ) ;
#29147=CARTESIAN_POINT ( 'NONE',  ( 5.204170427930421283E-15, 0.000000000000000000, -12.79999999999999893 ) ) ;
#29187=EDGE_LOOP ( 'NONE', ( #12512, #22934 ) ) ;
#29283=EDGE_CURVE ( 'NONE', #3543, #69389, #69854, .T. ) ;
#29427=DIRECTION ( 'NONE',  ( 1.000000000000000000, 0.000000000000000000, 0.000000000000000000 ) ) ;
#29493=EDGE_LOOP ( 'NONE', ( #240, #70336, #60624, #20179 ) ) ;
#29512=ADVANCED_FACE ( 'NONE', ( #31847 ), #20196, .T. ) ;
#29717=FACE_OUTER_BOUND ( 'NONE', #19305, .T. ) ;
#29750=CARTESIAN_POINT ( 'NONE',  ( -10.90093335751250692, 0.000000000000000000, -13.71399988598171049 ) ) ;
#29787=AXIS2_PLACEMENT_3D ( 'NONE', #44638, #67558, #54790 ) ;
#29942=ORIENTED_EDGE ( 'NONE', *, *, #44164, .T. ) ;
#30026=ORIENTED_EDGE ( 'NONE', *, *, #13888, .F. ) ;
#30101=DIRECTION ( 'NONE',  ( 0.000000000000000000, 0.000000000000000000, -1.000000000000000000 ) ) ;
#30106=AXIS2_PLACEMENT_3D ( 'NONE', #16694, #5062, #68198 ) ;
#30218=AXIS2_PLACEMENT_3D ( 'NONE', #46650, #35724, #18084 ) ;
#30273=CARTESIAN_POINT ( 'NONE',  ( -11.70000000000000107, 0.000000000000000000, 0.000000000000000000 ) ) ;
#30279=EDGE_CURVE ( 'NONE', #32156, #16833, #14289, .T. ) ;
#30298=EDGE_CURVE ( 'NONE', #65590, #18520, #53042, .T. ) ;
#30302=EDGE_LOOP ( 'NONE', ( #42029, #5097, #1448, #54199 ) ) ;
#30425=VERTEX_POINT ( 'NONE', #33423 ) ;
#30456=CIRCLE ( 'NONE', #49668, 13.90444123027096879 ) ;
#30565=DIRECTION ( 'NONE',  ( 0.9781476007338070211, 2.546183866652750331E-17, 0.2079116908177527367 ) ) ;
#30836=FACE_OUTER_BOUND ( 'NONE', #11915, .T. ) ;
#30837=DIRECTION ( 'NONE',  ( 1.000000000000000000, 0.000000000000000000, 0.000000000000000000 ) ) ;
#30905=DIRECTION ( 'NONE',  ( -0.2079116908177527367, 1.197885328332319922E-16, -0.9781476007338070211 ) ) ;
#31073=CIRCLE ( 'NONE', #4708, 15.39727592608509177 ) ;
#31548=CARTESIAN_POINT ( 'NONE',  ( -0.2999999999999947153, 0.000000000000000000, -12.50000000000000000 ) ) ;
#31562=ADVANCED_FACE ( 'NONE', ( #5731 ), #69604, .T. ) ;
#31607=FILL_AREA_STYLE_COLOUR ( '', #8014 ) ;
#31790=ORIENTED_EDGE ( 'NONE', *, *, #30298, .T. ) ;
#31824=FACE_OUTER_BOUND ( 'NONE', #26345, .T. ) ;
#31847=FACE_OUTER_BOUND ( 'NONE', #1073, .T. ) ;
#32051=DIRECTION ( 'NONE',  ( 1.000000000000000000, 0.000000000000000000, 0.000000000000000000 ) ) ;
#32085=CYLINDRICAL_SURFACE ( 'NONE', #7228, 15.77977592589476608 ) ;
#32156=VERTEX_POINT ( 'NONE', #67860 ) ;
#32178=ORIENTED_EDGE ( 'NONE', *, *, #28273, .F. ) ;
#32184=DIRECTION ( 'NONE',  ( 1.000000000000000000, -0.000000000000000000, -0.000000000000000000 ) ) ;
#32315=ADVANCED_FACE ( 'NONE', ( #40393 ), #63341, .T. ) ;
#32408=DIRECTION ( 'NONE',  ( 0.000000000000000000, 0.000000000000000000, -1.000000000000000000 ) ) ;
#32543=VECTOR ( 'NONE', #16147, 1000.000000000000114 ) ;
#32618=COLOUR_RGB ( '', 0.08235294, 0.09019608, 0.10196078) ;
#32924=CARTESIAN_POINT ( 'NONE',  ( -3.360000000000002096, 0.000000000000000000, 0.000000000000000000 ) ) ;
#33423=CARTESIAN_POINT ( 'NONE',  ( 5.204170427930421283E-15, 1.567547902908612184E-15, 12.79999999999999893 ) ) ;
#33484=DIRECTION ( 'NONE',  ( 0.000000000000000000, 0.000000000000000000, -1.000000000000000000 ) ) ;
#33529=CARTESIAN_POINT ( 'NONE',  ( -11.70000000000000107, 0.000000000000000000, 0.000000000000000000 ) ) ;
#33714=EDGE_CURVE ( 'NONE', #30425, #20114, #39602, .T. ) ;
#33824=CIRCLE ( 'NONE', #42221, 13.90444123027096879 ) ;
#34003=EDGE_LOOP ( 'NONE', ( #23028, #3939 ) ) ;
#34033=CYLINDRICAL_SURFACE ( 'NONE', #46220, 20.99999999999999645 ) ;
#34056=CARTESIAN_POINT ( 'NONE',  ( -3.000000000000002665, 0.000000000000000000, 0.000000000000000000 ) ) ;
#34117=DIRECTION ( 'NONE',  ( 0.000000000000000000, 1.224646799147353207E-16, 1.000000000000000000 ) ) ;
#34229=AXIS2_PLACEMENT_3D ( 'NONE', #30273, #70478, #64878 ) ;
#34755=ORIENTED_EDGE ( 'NONE', *, *, #19374, .T. ) ;
#34828=AXIS2_PLACEMENT_3D ( 'NONE', #7466, #24748, #7832 ) ;
#34860=ORIENTED_EDGE ( 'NONE', *, *, #60813, .T. ) ;
#34916=CARTESIAN_POINT ( 'NONE',  ( -11.69999999999999929, 2.571758278209441267E-15, 20.99999999999999645 ) ) ;
#35000=EDGE_CURVE ( 'NONE', #67617, #16833, #62019, .T. ) ;
#35091=EDGE_CURVE ( 'NONE', #73994, #35854, #69751, .T. ) ;
#35147=DIRECTION ( 'NONE',  ( 1.000000000000000000, -0.000000000000000000, -0.000000000000000000 ) ) ;
#35163=LINE ( 'NONE', #28781, #14662 ) ;
#35195=DIRECTION ( 'NONE',  ( -0.2079116908177587875, 0.000000000000000000, 0.9781476007338056888 ) ) ;
#35248=DIRECTION ( 'NONE',  ( -1.000000000000000000, -0.000000000000000000, -0.000000000000000000 ) ) ;
#35390=FACE_OUTER_BOUND ( 'NONE', #44523, .T. ) ;
#35492=EDGE_CURVE ( 'NONE', #69389, #73994, #57767, .T. ) ;
#35499=EDGE_CURVE ( 'NONE', #41023, #30425, #25379, .T. ) ;
#35589=ORIENTED_EDGE ( 'NONE', *, *, #35000, .T. ) ;
#35611=DIRECTION ( 'NONE',  ( 0.000000000000000000, 0.000000000000000000, -1.000000000000000000 ) ) ;
#35724=DIRECTION ( 'NONE',  ( -1.000000000000000000, -0.000000000000000000, -0.000000000000000000 ) ) ;
#35739=DIRECTION ( 'NONE',  ( 0.000000000000000000, 0.000000000000000000, 1.000000000000000000 ) ) ;
#35854=VERTEX_POINT ( 'NONE', #3966 ) ;
#35873=CARTESIAN_POINT ( 'NONE',  ( -11.99999999999999645, 0.000000000000000000, 12.85999999999999943 ) ) ;
#35880=CIRCLE ( 'NONE', #3498, 13.71399988598171049 ) ;
#35978=VERTEX_POINT ( 'NONE', #71616 ) ;
#36030=DIRECTION ( 'NONE',  ( 1.000000000000000000, 0.000000000000000000, 0.000000000000000000 ) ) ;
#36118=ORIENTED_EDGE ( 'NONE', *, *, #64101, .T. ) ;
#36177=DIRECTION ( 'NONE',  ( -1.000000000000000000, 0.000000000000000000, -0.000000000000000000 ) ) ;
#36203=AXIS2_PLACEMENT_3D ( 'NONE', #25441, #3279, #20158 ) ;
#36266=EDGE_CURVE ( 'NONE', #68149, #7348, #18911, .T. ) ;
#36577=AXIS2_PLACEMENT_3D ( 'NONE', #8151, #48013, #70926 ) ;
#36588=EDGE_LOOP ( 'NONE', ( #32178, #43312, #53371, #23030 ) ) ;
#36644=EDGE_CURVE ( 'NONE', #26896, #23517, #20161, .T. ) ;
#36658=FACE_OUTER_BOUND ( 'NONE', #20888, .T. ) ;
#36916=FACE_OUTER_BOUND ( 'NONE', #5352, .T. ) ;
#36947=DIRECTION ( 'NONE',  ( 0.000000000000000000, 1.224646799147347784E-16, 1.000000000000000000 ) ) ;
#36950=FILL_AREA_STYLE_COLOUR ( '', #32618 ) ;
#37018=AXIS2_PLACEMENT_3D ( 'NONE', #64001, #15628, #69629 ) ;
#37045=VECTOR ( 'NONE', #69439, 1000.000000000000000 ) ;
#37077=PRODUCT_DEFINITION ( 'UNKNOWN', '', #25660, #48410 ) ;
#37205=EDGE_CURVE ( 'NONE', #41131, #24664, #60374, .T. ) ;
#37210=EDGE_LOOP ( 'NONE', ( #26625, #69002, #53239, #64472 ) ) ;
#37283=VECTOR ( 'NONE', #30905, 1000.000000000000000 ) ;
#37309=CARTESIAN_POINT ( 'NONE',  ( -2.977765906491215642, 15.77977592589476608, 0.000000000000000000 ) ) ;
#37433=ORIENTED_EDGE ( 'NONE', *, *, #70672, .F. ) ;
#37536=EDGE_CURVE ( 'NONE', #41131, #68149, #49887, .T. ) ;
#37691=CARTESIAN_POINT ( 'NONE',  ( -0.2999999999999964362, 0.000000000000000000, 0.000000000000000000 ) ) ;
#37702=SURFACE_SIDE_STYLE ('',( #19283 ) ) ;
#37704=CONICAL_SURFACE ( 'NONE', #67693, 17.45460580326810174, 1.361356816555583826 ) ;
#37809=DIRECTION ( 'NONE',  ( -0.2079116908177431888, 1.197885328332322634E-16, -0.9781476007338091305 ) ) ;
#37907=ORIENTED_EDGE ( 'NONE', *, *, #20454, .F. ) ;
#37971=PRODUCT ( 'taper roller bearing_iso_ISO 355-2 - 2BD25 - 22,SI,NC,22', 'taper roller bearing_iso_ISO 355-2 - 2BD25 - 22,SI,NC,22', '', ( #887 ) ) ;
#38003=ORIENTED_EDGE ( 'NONE', *, *, #48192, .F. ) ;
#38059=DIRECTION ( 'NONE',  ( 0.000000000000000000, 0.000000000000000000, 1.000000000000000000 ) ) ;
#38062=AXIS2_PLACEMENT_3D ( 'NONE', #41064, #62908, #24149 ) ;
#38131=DIRECTION ( 'NONE',  ( 1.000000000000000000, 0.000000000000000000, 0.000000000000000000 ) ) ;
#38340=CIRCLE ( 'NONE', #7099, 12.79999999999999893 ) ;
#38386=DIRECTION ( 'NONE',  ( 1.000000000000000000, 0.000000000000000000, 0.000000000000000000 ) ) ;
#38675=EDGE_LOOP ( 'NONE', ( #4912, #41053, #60066, #72139 ) ) ;
#38741=VERTEX_POINT ( 'NONE', #65283 ) ;
#38773=CARTESIAN_POINT ( 'NONE',  ( -3.000000000000002665, 0.000000000000000000, 0.000000000000000000 ) ) ;
#38783=EDGE_CURVE ( 'NONE', #28467, #26369, #17645, .T. ) ;
#38823=VERTEX_POINT ( 'NONE', #19399 ) ;
#38966=CARTESIAN_POINT ( 'NONE',  ( -10.90076147243505211, 1.679431090506078290E-15, -13.71319123027096865 ) ) ;
#39105=ORIENTED_EDGE ( 'NONE', *, *, #35492, .T. ) ;
#39114=ORIENTED_EDGE ( 'NONE', *, *, #7378, .T. ) ;
#39234=ORIENTED_EDGE ( 'NONE', *, *, #35492, .F. ) ;
#39428=VECTOR ( 'NONE', #55907, 1000.000000000000114 ) ;
#39602=CIRCLE ( 'NONE', #25156, 0.2999999999999999334 ) ;
#39645=EDGE_CURVE ( 'NONE', #26369, #28467, #14131, .T. ) ;
#39727=EDGE_CURVE ( 'NONE', #16833, #3451, #74248, .T. ) ;
#39800=CARTESIAN_POINT ( 'NONE',  ( -11.68233973192911535, 0.000000000000000000, 0.000000000000000000 ) ) ;
#39936=FACE_OUTER_BOUND ( 'NONE', #12286, .T. ) ;
#39956=ORIENTED_EDGE ( 'NONE', *, *, #35091, .F. ) ;
#39968=CARTESIAN_POINT ( 'NONE',  ( -11.99999999999999645, 0.000000000000000000, 0.000000000000000000 ) ) ;
#40239=ORIENTED_EDGE ( 'NONE', *, *, #60813, .F. ) ;
#40328=DIRECTION ( 'NONE',  ( 1.000000000000000000, 0.000000000000000000, 0.000000000000000000 ) ) ;
#40393=FACE_OUTER_BOUND ( 'NONE', #36588, .T. ) ;
#40429=CIRCLE ( 'NONE', #51204, 20.64000000000000057 ) ;
#40546=CONICAL_SURFACE ( 'NONE', #4548, 15.39727592608509177, 1.361356816555577609 ) ;
#40663=DIRECTION ( 'NONE',  ( 0.000000000000000000, 0.000000000000000000, -1.000000000000000000 ) ) ;
#40706=DIRECTION ( 'NONE',  ( 0.000000000000000000, 0.000000000000000000, -1.000000000000000000 ) ) ;
#40708=CONICAL_SURFACE ( 'NONE', #47887, 12.85999999999999943, 0.7853981633974482790 ) ;
#40813=CARTESIAN_POINT ( 'NONE',  ( -10.90093335751250692, 1.782551537117168429E-15, 13.71399988598171049 ) ) ;
#40818=AXIS2_PLACEMENT_3D ( 'NONE', #53858, #13629, #67642 ) ;
#40895=ORIENTED_EDGE ( 'NONE', *, *, #19374, .F. ) ;
#40902=DIRECTION ( 'NONE',  ( 0.000000000000000000, -1.000000000000000000, 0.000000000000000000 ) ) ;
#41003=FACE_OUTER_BOUND ( 'NONE', #27068, .T. ) ;
#41023=VERTEX_POINT ( 'NONE', #29147 ) ;
#41053=ORIENTED_EDGE ( 'NONE', *, *, #50984, .T. ) ;
#41064=CARTESIAN_POINT ( 'NONE',  ( -11.69999999999999929, 0.000000000000000000, 0.000000000000000000 ) ) ;
#41131=VERTEX_POINT ( 'NONE', #38966 ) ;
#41448=ORIENTED_EDGE ( 'NONE', *, *, #45583, .F. ) ;
#41624=FACE_OUTER_BOUND ( 'NONE', #7769, .T. ) ;
#41636=ORIENTED_EDGE ( 'NONE', *, *, #11386, .F. ) ;
#41789=( NAMED_UNIT ( * ) SI_UNIT ( $, .STERADIAN. ) SOLID_ANGLE_UNIT ( ) );
#41823=LINE ( 'NONE', #64769, #14621 ) ;
#41856=CARTESIAN_POINT ( 'NONE',  ( -2.977765906491215642, 1.885622467823562354E-15, 15.39727592589476579 ) ) ;
#41956=AXIS2_PLACEMENT_3D ( 'NONE', #13146, #7520, #59393 ) ;
#41965=AXIS2_PLACEMENT_3D ( 'NONE', #24119, #48149, #30101 ) ;
#42029=ORIENTED_EDGE ( 'NONE', *, *, #60922, .F. ) ;
#42072=ORIENTED_EDGE ( 'NONE', *, *, #60922, .T. ) ;
#42076=ORIENTED_EDGE ( 'NONE', *, *, #48192, .T. ) ;
#42128=SHAPE_REPRESENTATION ( 'taper roller bearing_iso_ISO 355-2 - 2BD25 - 22,SI,NC,22', ( #43395 ), #57869 ) ;
#42221=AXIS2_PLACEMENT_3D ( 'NONE', #12677, #1455, #709 ) ;
#42268=CONICAL_SURFACE ( 'NONE', #53051, 13.71319123046128752, 0.2094395102393127317 ) ;
#42305=ORIENTED_EDGE ( 'NONE', *, *, #35000, .F. ) ;
#42379=EDGE_LOOP ( 'NONE', ( #1259, #50191 ) ) ;
#42387=ADVANCED_FACE ( 'NONE', ( #36658 ), #4248, .F. ) ;
#42401=CYLINDRICAL_SURFACE ( 'NONE', #59174, 12.50000000000000000 ) ;
#42443=EDGE_LOOP ( 'NONE', ( #1146, #35589, #69720, #58461 ) ) ;
#42611=ORIENTED_EDGE ( 'NONE', *, *, #70672, .T. ) ;
#42704=VECTOR ( 'NONE', #68799, 1000.000000000000000 ) ;
#42754=DIRECTION ( 'NONE',  ( 0.000000000000000000, 0.000000000000000000, -1.000000000000000000 ) ) ;
#42938=ORIENTED_EDGE ( 'NONE', *, *, #33714, .T. ) ;
#43096=DIRECTION ( 'NONE',  ( 1.000000000000000000, 0.000000000000000000, 0.000000000000000000 ) ) ;
#43226=FACE_OUTER_BOUND ( 'NONE', #30302, .T. ) ;
#43297=PRESENTATION_STYLE_ASSIGNMENT (( #19956 ) ) ;
#43312=ORIENTED_EDGE ( 'NONE', *, *, #20454, .T. ) ;
#43317=CARTESIAN_POINT ( 'NONE',  ( -11.99999999999999645, 13.90444123027096879, 0.000000000000000000 ) ) ;
#43324=DIRECTION ( 'NONE',  ( 1.000000000000000000, 0.000000000000000000, 0.000000000000000000 ) ) ;
#43339=CARTESIAN_POINT ( 'NONE',  ( -3.000000000000002665, 0.000000000000000000, 0.000000000000000000 ) ) ;
#43395=AXIS2_PLACEMENT_3D ( 'NONE', #48320, #71232, #19735 ) ;
#43439=ORIENTED_EDGE ( 'NONE', *, *, #28436, .T. ) ;
#43679=PLANE ( 'NONE',  #61138 ) ;
#43702=CIRCLE ( 'NONE', #7670, 12.50000000000000000 ) ;
#43766=DIRECTION ( 'NONE',  ( 1.000000000000000000, 0.000000000000000000, 0.000000000000000000 ) ) ;
#43832=EDGE_CURVE ( 'NONE', #68149, #41131, #46677, .T. ) ;
#43886=EDGE_CURVE ( 'NONE', #24664, #3543, #35880, .T. ) ;
#44080=CIRCLE ( 'NONE', #17671, 12.50000000000000000 ) ;
#44146=CARTESIAN_POINT ( 'NONE',  ( -11.69999999999999929, 0.000000000000000000, 0.000000000000000000 ) ) ;
#44152=ADVANCED_FACE ( 'NONE', ( #30836 ), #25223, .T. ) ;
#44164=EDGE_CURVE ( 'NONE', #32156, #35978, #11891, .T. ) ;
#44451=DIRECTION ( 'NONE',  ( 0.000000000000000000, 0.000000000000000000, -1.000000000000000000 ) ) ;
#44483=ORIENTED_EDGE ( 'NONE', *, *, #71050, .T. ) ;
#44523=EDGE_LOOP ( 'NONE', ( #47293, #39114, #62449, #5024 ) ) ;
#44578=ADVANCED_FACE ( 'NONE', ( #18365, #12721 ), #70594, .T. ) ;
#44612=ORIENTED_EDGE ( 'NONE', *, *, #44164, .F. ) ;
#44638=CARTESIAN_POINT ( 'NONE',  ( -42.50000000000000000, 0.000000000000000000, 0.000000000000000000 ) ) ;
#44804=CARTESIAN_POINT ( 'NONE',  ( -2.977765906491215642, 0.000000000000000000, -15.77977592589476608 ) ) ;
#44966=ORIENTED_EDGE ( 'NONE', *, *, #49642, .F. ) ;
#45120=EDGE_LOOP ( 'NONE', ( #40895, #28834, #21246, #34860 ) ) ;
#45234=ADVANCED_FACE ( 'NONE', ( #67384 ), #98, .T. ) ;
#45272=DIRECTION ( 'NONE',  ( 0.000000000000000000, 0.000000000000000000, -1.000000000000000000 ) ) ;
#45338=EDGE_CURVE ( 'NONE', #55509, #69802, #28263, .T. ) ;
#45374=ADVANCED_FACE ( 'NONE', ( #39936 ), #1276, .T. ) ;
#45400=CONICAL_SURFACE ( 'NONE', #20148, 20.64000000000000057, 0.7853981633974482790 ) ;
#45446=CIRCLE ( 'NONE', #70566, 20.99999999999999645 ) ;
#45449=DIRECTION ( 'NONE',  ( -0.7071067811865474617, 8.659560562354932858E-17, -0.7071067811865474617 ) ) ;
#45583=EDGE_CURVE ( 'NONE', #54917, #7348, #26322, .T. ) ;
#45587=DIRECTION ( 'NONE',  ( -1.000000000000000000, 0.000000000000000000, 0.000000000000000000 ) ) ;
#45906=EDGE_LOOP ( 'NONE', ( #65838, #36118, #72215, #37433 ) ) ;
#46037=AXIS2_PLACEMENT_3D ( 'NONE', #51451, #22905, #22149 ) ;
#46203=ADVANCED_FACE ( 'NONE', ( #69358 ), #70086, .F. ) ;
#46220=AXIS2_PLACEMENT_3D ( 'NONE', #5489, #67134, #51320 ) ;
#46336=ORIENTED_EDGE ( 'NONE', *, *, #63488, .F. ) ;
#46502=CARTESIAN_POINT ( 'NONE',  ( -10.90076147243505211, 0.000000000000000000, 13.71319123027096865 ) ) ;
#46543=ADVANCED_FACE ( 'NONE', ( #9163 ), #32085, .T. ) ;
#46604=FACE_OUTER_BOUND ( 'NONE', #50961, .T. ) ;
#46650=CARTESIAN_POINT ( 'NONE',  ( -10.90076147243505211, 0.000000000000000000, 0.000000000000000000 ) ) ;
#46677=CIRCLE ( 'NONE', #57528, 13.71319123027096865 ) ;
#46679=CARTESIAN_POINT ( 'NONE',  ( -42.50000000000000000, 0.000000000000000000, -15.77977592589476608 ) ) ;
#46794=DIRECTION ( 'NONE',  ( 0.000000000000000000, 0.000000000000000000, -1.000000000000000000 ) ) ;
#46939=EDGE_CURVE ( 'NONE', #5475, #58812, #66597, .T. ) ;
#46986=DIRECTION ( 'NONE',  ( -0.000000000000000000, 0.000000000000000000, 1.000000000000000000 ) ) ;
#47155=DIRECTION ( 'NONE',  ( 1.000000000000000000, 0.000000000000000000, 0.000000000000000000 ) ) ;
#47160=CARTESIAN_POINT ( 'NONE',  ( -10.94538922500103162, 0.000000000000000000, 0.000000000000000000 ) ) ;
#47293=ORIENTED_EDGE ( 'NONE', *, *, #20877, .F. ) ;
#47410=FACE_OUTER_BOUND ( 'NONE', #24941, .T. ) ;
#47411=DIRECTION ( 'NONE',  ( 1.000000000000000000, 0.000000000000000000, 0.000000000000000000 ) ) ;
#47424=ADVANCED_FACE ( 'NONE', ( #43226 ), #60162, .T. ) ;
#47438=SURFACE_STYLE_FILL_AREA ( #7583 ) ;
#47638=CARTESIAN_POINT ( 'NONE',  ( -0.2999999999999964362, 0.000000000000000000, -12.80000000000000071 ) ) ;
#47793=VECTOR ( 'NONE', #17956, 1000.000000000000000 ) ;
#47824=CARTESIAN_POINT ( 'NONE',  ( 6.938893903907228378E-15, 0.000000000000000000, 0.000000000000000000 ) ) ;
#47852=CARTESIAN_POINT ( 'NONE',  ( -10.90473778262209414, 0.000000000000000000, -13.71319123046128752 ) ) ;
#47887=AXIS2_PLACEMENT_3D ( 'NONE', #69956, #18455, #35739 ) ;
#48013=DIRECTION ( 'NONE',  ( 1.000000000000000000, 0.000000000000000000, 0.000000000000000000 ) ) ;
#48063=EDGE_CURVE ( 'NONE', #55509, #21370, #19391, .T. ) ;
#48149=DIRECTION ( 'NONE',  ( 1.000000000000000000, 0.000000000000000000, 0.000000000000000000 ) ) ;
#48192=EDGE_CURVE ( 'NONE', #21370, #49839, #41823, .T. ) ;
#48194=DIRECTION ( 'NONE',  ( -1.000000000000000000, 0.000000000000000000, -0.000000000000000000 ) ) ;
#48320=CARTESIAN_POINT ( 'NONE',  ( 0.000000000000000000, 0.000000000000000000, 0.000000000000000000 ) ) ;
#48410=PRODUCT_DEFINITION_CONTEXT ( 'detailed design', #59957, 'design' ) ;
#48442=DIRECTION ( 'NONE',  ( 0.000000000000000000, 0.000000000000000000, -1.000000000000000000 ) ) ;
#48920=DIRECTION ( 'NONE',  ( -0.7071067811865474617, 0.000000000000000000, 0.7071067811865474617 ) ) ;
#48929=FACE_OUTER_BOUND ( 'NONE', #64083, .T. ) ;
#49006=DIRECTION ( 'NONE',  ( 0.000000000000000000, 0.000000000000000000, -1.000000000000000000 ) ) ;
#49144=DIRECTION ( 'NONE',  ( 1.000000000000000000, 0.000000000000000000, 0.000000000000000000 ) ) ;
#49176=AXIS2_PLACEMENT_3D ( 'NONE', #54772, #54403, #42754 ) ;
#49452=VECTOR ( 'NONE', #30565, 1000.000000000000000 ) ;
#49642=EDGE_CURVE ( 'NONE', #3543, #24664, #1626, .T. ) ;
#49656=ADVANCED_FACE ( 'NONE', ( #21770 ), #4027, .T. ) ;
#49668=AXIS2_PLACEMENT_3D ( 'NONE', #39968, #40328, #40706 ) ;
#49682=DIRECTION ( 'NONE',  ( 1.000000000000000000, 0.000000000000000000, 0.000000000000000000 ) ) ;
#49730=CARTESIAN_POINT ( 'NONE',  ( -12.00000000000000000, 17.30399999999999849, 0.000000000000000000 ) ) ;
#49808=ORIENTED_EDGE ( 'NONE', *, *, #24948, .F. ) ;
#49812=ORIENTED_EDGE ( 'NONE', *, *, #29283, .F. ) ;
#49839=VERTEX_POINT ( 'NONE', #58572 ) ;
#49887=CIRCLE ( 'NONE', #55912, 13.71319123027096865 ) ;
#49937=ORIENTED_EDGE ( 'NONE', *, *, #35499, .T. ) ;
#49966=AXIS2_PLACEMENT_3D ( 'NONE', #37309, #36177, #65507 ) ;
#50086=LINE ( 'NONE', #13390, #64798 ) ;
#50091=AXIS2_PLACEMENT_3D ( 'NONE', #49730, #50096, #46986 ) ;
#50096=DIRECTION ( 'NONE',  ( -1.000000000000000000, 0.000000000000000000, -0.000000000000000000 ) ) ;
#50170=AXIS2_PLACEMENT_3D ( 'NONE', #66124, #65381, #48442 ) ;
#50191=ORIENTED_EDGE ( 'NONE', *, *, #38783, .F. ) ;
#50344=AXIS2_PLACEMENT_3D ( 'NONE', #7609, #13971, #65138 ) ;
#50381=DIRECTION ( 'NONE',  ( 1.000000000000000000, 0.000000000000000000, 0.000000000000000000 ) ) ;
#50422=ORIENTED_EDGE ( 'NONE', *, *, #13414, .F. ) ;
#50438=LINE ( 'NONE', #67362, #8835 ) ;
#50442=CARTESIAN_POINT ( 'NONE',  ( 6.938893903907228378E-15, 0.000000000000000000, -15.77977592589476608 ) ) ;
#50681=ORIENTED_EDGE ( 'NONE', *, *, #43832, .T. ) ;
#50692=ORIENTED_EDGE ( 'NONE', *, *, #13888, .T. ) ;
#50749=ORIENTED_EDGE ( 'NONE', *, *, #14277, .T. ) ;
#50936=CARTESIAN_POINT ( 'NONE',  ( -2.981742216678212820, 0.000000000000000000, 0.000000000000000000 ) ) ;
#50961=EDGE_LOOP ( 'NONE', ( #67775, #8239, #24584, #18463 ) ) ;
#50984=EDGE_CURVE ( 'NONE', #28467, #56010, #18536, .T. ) ;
#51019=CARTESIAN_POINT ( 'NONE',  ( -11.99999999999999645, 0.000000000000000000, -13.90444123027096879 ) ) ;
#51068=DIRECTION ( 'NONE',  ( 0.000000000000000000, 0.000000000000000000, 1.000000000000000000 ) ) ;
#51077=CARTESIAN_POINT ( 'NONE',  ( -11.63999999999999702, 1.552852141318844077E-15, -12.50000000000000000 ) ) ;
#51131=CARTESIAN_POINT ( 'NONE',  ( -11.99999999999999645, 0.000000000000000000, 0.000000000000000000 ) ) ;
#51204=AXIS2_PLACEMENT_3D ( 'NONE', #38773, #68090, #33484 ) ;
#51320=DIRECTION ( 'NONE',  ( 0.000000000000000000, 0.000000000000000000, -1.000000000000000000 ) ) ;
#51451=CARTESIAN_POINT ( 'NONE',  ( -10.90076147243505211, 0.000000000000000000, 0.000000000000000000 ) ) ;
#51570=DIRECTION ( 'NONE',  ( 1.000000000000000000, 0.000000000000000000, 0.000000000000000000 ) ) ;
#51581=AXIS2_PLACEMENT_3D ( 'NONE', #8351, #71114, #71484 ) ;
#51668=AXIS2_PLACEMENT_3D ( 'NONE', #33529, #55733, #9868 ) ;
#51689=DIRECTION ( 'NONE',  ( 1.000000000000000000, 0.000000000000000000, 0.000000000000000000 ) ) ;
#51735=ORIENTED_EDGE ( 'NONE', *, *, #6649, .T. ) ;
#51736=CARTESIAN_POINT ( 'NONE',  ( -12.00000000000000000, 2.123263276254396040E-15, 17.30399999999999849 ) ) ;
#51848=DIRECTION ( 'NONE',  ( 0.000000000000000000, 0.000000000000000000, -1.000000000000000000 ) ) ;
#51874=UNCERTAINTY_MEASURE_WITH_UNIT (LENGTH_MEASURE( 1.000000000000000082E-05 ), #64731, 'distance_accuracy_value', 'NONE');
#52115=DIRECTION ( 'NONE',  ( 0.000000000000000000, 0.000000000000000000, -1.000000000000000000 ) ) ;
#52308=DIRECTION ( 'NONE',  ( 0.000000000000000000, 0.000000000000000000, -1.000000000000000000 ) ) ;
#52405=DIRECTION ( 'NONE',  ( 0.000000000000000000, 0.000000000000000000, -1.000000000000000000 ) ) ;
#52424=DIRECTION ( 'NONE',  ( 0.000000000000000000, 0.000000000000000000, -1.000000000000000000 ) ) ;
#52563=CARTESIAN_POINT ( 'NONE',  ( -42.50000000000000000, 0.000000000000000000, 0.000000000000000000 ) ) ;
#52595=ORIENTED_EDGE ( 'NONE', *, *, #15186, .F. ) ;
#53042=LINE ( 'NONE', #20298, #2313 ) ;
#53051=AXIS2_PLACEMENT_3D ( 'NONE', #1358, #35147, #52424 ) ;
#53239=ORIENTED_EDGE ( 'NONE', *, *, #43886, .T. ) ;
#53371=ORIENTED_EDGE ( 'NONE', *, *, #62590, .T. ) ;
#53490=LINE ( 'NONE', #70386, #10584 ) ;
#53521=CARTESIAN_POINT ( 'NONE',  ( -3.000000000000002665, 0.000000000000000000, -19.21700905503013601 ) ) ;
#53660=AXIS2_PLACEMENT_3D ( 'NONE', #966, #51689, #236 ) ;
#53828=DIRECTION ( 'NONE',  ( -0.000000000000000000, 0.000000000000000000, 1.000000000000000000 ) ) ;
#53832=ORIENTED_EDGE ( 'NONE', *, *, #29283, .T. ) ;
#53858=CARTESIAN_POINT ( 'NONE',  ( -0.2999999999999964362, 0.000000000000000000, 0.000000000000000000 ) ) ;
#53907=EDGE_CURVE ( 'NONE', #69802, #49839, #12858, .T. ) ;
#53914=EDGE_LOOP ( 'NONE', ( #60076, #44483, #12476, #71374 ) ) ;
#53932=AXIS2_PLACEMENT_3D ( 'NONE', #71060, #19200, #59805 ) ;
#54159=CARTESIAN_POINT ( 'NONE',  ( -12.00000000000000000, 0.000000000000000000, -17.30399999999999849 ) ) ;
#54199=ORIENTED_EDGE ( 'NONE', *, *, #30298, .F. ) ;
#54217=ADVANCED_FACE ( 'NONE', ( #5018, #26805 ), #15905, .T. ) ;
#54403=DIRECTION ( 'NONE',  ( 1.000000000000000000, 0.000000000000000000, 0.000000000000000000 ) ) ;
#54515=CONICAL_SURFACE ( 'NONE', #28098, 17.30399999999999849, 0.2094395102393129815 ) ;
#54540=ORIENTED_EDGE ( 'NONE', *, *, #56809, .T. ) ;
#54560=CIRCLE ( 'NONE', #36577, 21.00000000000000000 ) ;
#54588=CARTESIAN_POINT ( 'NONE',  ( -2.977765906491215642, 0.000000000000000000, 0.000000000000000000 ) ) ;
#54615=CARTESIAN_POINT ( 'NONE',  ( -10.90076147243505211, 0.000000000000000000, 0.000000000000000000 ) ) ;
#54761=CARTESIAN_POINT ( 'NONE',  ( -3.360000000000002096, 2.571758278209441661E-15, 21.00000000000000000 ) ) ;
#54772=CARTESIAN_POINT ( 'NONE',  ( -2.977765906491215642, 0.000000000000000000, 0.000000000000000000 ) ) ;
#54774=CIRCLE ( 'NONE', #24762, 19.21700905503013601 ) ;
#54787=DIRECTION ( 'NONE',  ( 0.000000000000000000, 0.000000000000000000, -1.000000000000000000 ) ) ;
#54790=DIRECTION ( 'NONE',  ( 0.000000000000000000, 0.000000000000000000, -1.000000000000000000 ) ) ;
#54893=ADVANCED_FACE ( 'NONE', ( #72402 ), #56674, .T. ) ;
#54907=CIRCLE ( 'NONE', #18897, 12.50000000000000000 ) ;
#54917=VERTEX_POINT ( 'NONE', #28770 ) ;
#55026=CARTESIAN_POINT ( 'NONE',  ( -42.50000000000000000, 0.000000000000000000, 0.000000000000000000 ) ) ;
#55135=ORIENTED_EDGE ( 'NONE', *, *, #5294, .F. ) ;
#55347=CARTESIAN_POINT ( 'NONE',  ( -2.977765906491215642, 0.000000000000000000, 0.000000000000000000 ) ) ;
#55357=AXIS2_PLACEMENT_3D ( 'NONE', #34056, #66148, #5508 ) ;
#55422=VECTOR ( 'NONE', #35195, 1000.000000000000114 ) ;
#55509=VERTEX_POINT ( 'NONE', #44804 ) ;
#55572=ORIENTED_EDGE ( 'NONE', *, *, #63488, .T. ) ;
#55576=EDGE_CURVE ( 'NONE', #66054, #69389, #11149, .T. ) ;
#55733=DIRECTION ( 'NONE',  ( 1.000000000000000000, 0.000000000000000000, 0.000000000000000000 ) ) ;
#55874=DIRECTION ( 'NONE',  ( 1.000000000000000000, 0.000000000000000000, 0.000000000000000000 ) ) ;
#55907=DIRECTION ( 'NONE',  ( 0.9781476007338069101, 0.000000000000000000, -0.2079116908177528755 ) ) ;
#55912=AXIS2_PLACEMENT_3D ( 'NONE', #60650, #32051, #72275 ) ;
#55967=CARTESIAN_POINT ( 'NONE',  ( -3.000000000000002665, 2.527670993440137339E-15, -20.64000000000000057 ) ) ;
#56010=VERTEX_POINT ( 'NONE', #34916 ) ;
#56205=ADVANCED_FACE ( 'NONE', ( #18348 ), #42401, .F. ) ;
#56274=CARTESIAN_POINT ( 'NONE',  ( -11.99999999999999645, 1.702802944658382841E-15, 13.90444123027096879 ) ) ;
#56349=EDGE_LOOP ( 'NONE', ( #58804, #27553, #42611, #61615 ) ) ;
#56508=ORIENTED_EDGE ( 'NONE', *, *, #45338, .T. ) ;
#56559=PLANE ( 'NONE',  #30106 ) ;
#56674=CONICAL_SURFACE ( 'NONE', #36203, 15.39727592589476579, 0.2094395102393128150 ) ;
#56735=CARTESIAN_POINT ( 'NONE',  ( -11.63999999999999702, 0.000000000000000000, 0.000000000000000000 ) ) ;
#56809=EDGE_CURVE ( 'NONE', #19812, #3451, #50438, .T. ) ;
#56816=ORIENTED_EDGE ( 'NONE', *, *, #38783, .T. ) ;
#57144=LINE ( 'NONE', #22181, #42704 ) ;
#57427=CARTESIAN_POINT ( 'NONE',  ( -42.50000000000000000, 0.000000000000000000, -13.90444123027096879 ) ) ;
#57528=AXIS2_PLACEMENT_3D ( 'NONE', #54615, #9484, #32408 ) ;
#57767=LINE ( 'NONE', #22444, #55422 ) ;
#57769=AXIS2_PLACEMENT_3D ( 'NONE', #65705, #49144, #54787 ) ;
#57869=( GEOMETRIC_REPRESENTATION_CONTEXT ( 3 ) GLOBAL_UNCERTAINTY_ASSIGNED_CONTEXT ( ( #4620 ) ) GLOBAL_UNIT_ASSIGNED_CONTEXT ( ( #71885, #3137, #71516 ) ) REPRESENTATION_CONTEXT ( 'NONE', 'WORKASPACE' ) );
#57934=DIRECTION ( 'NONE',  ( 0.000000000000000000, 0.000000000000000000, -1.000000000000000000 ) ) ;
#58071=AXIS2_PLACEMENT_3D ( 'NONE', #55347, #16236, #44451 ) ;
#58179=DIRECTION ( 'NONE',  ( 0.000000000000000000, 0.000000000000000000, 1.000000000000000000 ) ) ;
#58182=CARTESIAN_POINT ( 'NONE',  ( -12.00000000000000000, 0.000000000000000000, 0.000000000000000000 ) ) ;
#58424=ORIENTED_EDGE ( 'NONE', *, *, #65471, .F. ) ;
#58461=ORIENTED_EDGE ( 'NONE', *, *, #56809, .F. ) ;
#58552=VERTEX_POINT ( 'NONE', #51019 ) ;
#58572=CARTESIAN_POINT ( 'NONE',  ( 6.938893903907228378E-15, 1.932465207890948911E-15, 15.77977592589476608 ) ) ;
#58804=ORIENTED_EDGE ( 'NONE', *, *, #64101, .F. ) ;
#58812=VERTEX_POINT ( 'NONE', #35873 ) ;
#58820=ORIENTED_EDGE ( 'NONE', *, *, #69495, .T. ) ;
#58936=ORIENTED_EDGE ( 'NONE', *, *, #28273, .T. ) ;
#59016=( NAMED_UNIT ( * ) SI_UNIT ( $, .STERADIAN. ) SOLID_ANGLE_UNIT ( ) );
#59057=CARTESIAN_POINT ( 'NONE',  ( -2.981742216678212820, 0.000000000000000000, 0.000000000000000000 ) ) ;
#59174=AXIS2_PLACEMENT_3D ( 'NONE', #52563, #24008, #25106 ) ;
#59393=DIRECTION ( 'NONE',  ( 0.000000000000000000, 0.000000000000000000, -1.000000000000000000 ) ) ;
#59542=AXIS2_PLACEMENT_3D ( 'NONE', #18878, #65875, #3469 ) ;
#59805=DIRECTION ( 'NONE',  ( 0.000000000000000000, 0.000000000000000000, 1.000000000000000000 ) ) ;
#59897=PRESENTATION_STYLE_ASSIGNMENT (( #9114 ) ) ;
#59957=APPLICATION_CONTEXT ( 'automotive_design' ) ;
#60066=ORIENTED_EDGE ( 'NONE', *, *, #13920, .F. ) ;
#60076=ORIENTED_EDGE ( 'NONE', *, *, #33714, .F. ) ;
#60162=CONICAL_SURFACE ( 'NONE', #55357, 20.64000000000000057, 0.7853981633974482790 ) ;
#60181=LINE ( 'NONE', #54159, #39428 ) ;
#60248=DIRECTION ( 'NONE',  ( 1.000000000000000000, 0.000000000000000000, 0.000000000000000000 ) ) ;
#60269=CARTESIAN_POINT ( 'NONE',  ( -12.00000000000000000, 2.119128821244579932E-15, 17.30399999999999849 ) ) ;
#60374=LINE ( 'NONE', #9959, #64716 ) ;
#60500=CIRCLE ( 'NONE', #58071, 15.77977592589476608 ) ;
#60521=CARTESIAN_POINT ( 'NONE',  ( -2.977765906491215642, 1.932465207890948911E-15, 15.77977592589476608 ) ) ;
#60568=AXIS2_PLACEMENT_3D ( 'NONE', #64792, #24560, #36947 ) ;
#60624=ORIENTED_EDGE ( 'NONE', *, *, #24284, .T. ) ;
#60650=CARTESIAN_POINT ( 'NONE',  ( -10.90076147243505211, 0.000000000000000000, 0.000000000000000000 ) ) ;
#60799=ORIENTED_EDGE ( 'NONE', *, *, #70095, .F. ) ;
#60801=ADVANCED_FACE ( 'NONE', ( #19987, #48929 ), #25280, .T. ) ;
#60813=EDGE_CURVE ( 'NONE', #61214, #20114, #17517, .T. ) ;
#60865=TOROIDAL_SURFACE ( 'NONE', #13997, 12.80000000000000071, 0.2999999999999999334 ) ;
#60922=EDGE_CURVE ( 'NONE', #20976, #65590, #40429, .T. ) ;
#61021=ORIENTED_EDGE ( 'NONE', *, *, #18442, .T. ) ;
#61138=AXIS2_PLACEMENT_3D ( 'NONE', #43317, #48194, #53828 ) ;
#61214=VERTEX_POINT ( 'NONE', #31548 ) ;
#61574=VERTEX_POINT ( 'NONE', #51077 ) ;
#61615=ORIENTED_EDGE ( 'NONE', *, *, #18570, .F. ) ;
#61744=CARTESIAN_POINT ( 'NONE',  ( -10.90093335751250692, 0.000000000000000000, 0.000000000000000000 ) ) ;
#61866=AXIS2_PLACEMENT_3D ( 'NONE', #21268, #32184, #2922 ) ;
#62019=LINE ( 'NONE', #60269, #32543 ) ;
#62147=ORIENTED_EDGE ( 'NONE', *, *, #18442, .F. ) ;
#62214=EDGE_CURVE ( 'NONE', #26369, #38741, #965, .T. ) ;
#62396=DIRECTION ( 'NONE',  ( 0.000000000000000000, 0.000000000000000000, -1.000000000000000000 ) ) ;
#62449=ORIENTED_EDGE ( 'NONE', *, *, #46939, .T. ) ;
#62590=EDGE_CURVE ( 'NONE', #58552, #35978, #24324, .T. ) ;
#62621=DIRECTION ( 'NONE',  ( 0.000000000000000000, 0.000000000000000000, -1.000000000000000000 ) ) ;
#62886=DIRECTION ( 'NONE',  ( 0.000000000000000000, 0.000000000000000000, 1.000000000000000000 ) ) ;
#62908=DIRECTION ( 'NONE',  ( 1.000000000000000000, 0.000000000000000000, 0.000000000000000000 ) ) ;
#63070=CIRCLE ( 'NONE', #6638, 21.00000000000000000 ) ;
#63176=DIRECTION ( 'NONE',  ( -1.000000000000000000, 0.000000000000000000, 0.000000000000000000 ) ) ;
#63341=CYLINDRICAL_SURFACE ( 'NONE', #4622, 13.90444123027096879 ) ;
#63415=CARTESIAN_POINT ( 'NONE',  ( 6.938893903907228378E-15, 0.000000000000000000, 0.000000000000000000 ) ) ;
#63416=ORIENTED_EDGE ( 'NONE', *, *, #13414, .T. ) ;
#63440=DIRECTION ( 'NONE',  ( -0.2079116908177431888, 0.000000000000000000, 0.9781476007338091305 ) ) ;
#63482=ORIENTED_EDGE ( 'NONE', *, *, #48063, .F. ) ;
#63488=EDGE_CURVE ( 'NONE', #49839, #69802, #17930, .T. ) ;
#63496=ADVANCED_FACE ( 'NONE', ( #14355 ), #63570, .F. ) ;
#63540=CARTESIAN_POINT ( 'NONE',  ( -11.70000000000000107, 0.000000000000000000, 0.000000000000000000 ) ) ;
#63570=CONICAL_SURFACE ( 'NONE', #50344, 17.30399999999999849, 0.2094395102393129815 ) ;
#63628=TOROIDAL_SURFACE ( 'NONE', #40818, 12.80000000000000071, 0.2999999999999999334 ) ;
#63737=DIRECTION ( 'NONE',  ( 1.000000000000000000, 0.000000000000000000, 0.000000000000000000 ) ) ;
#63802=AXIS2_PLACEMENT_3D ( 'NONE', #39800, #67619, #51068 ) ;
#63836=CARTESIAN_POINT ( 'NONE',  ( -3.000000000000002665, 0.000000000000000000, 0.000000000000000000 ) ) ;
#64001=CARTESIAN_POINT ( 'NONE',  ( -11.68233973192911535, 0.000000000000000000, 0.000000000000000000 ) ) ;
#64045=AXIS2_PLACEMENT_3D ( 'NONE', #20583, #67556, #66449 ) ;
#64083=EDGE_LOOP ( 'NONE', ( #63482, #21337 ) ) ;
#64101=EDGE_CURVE ( 'NONE', #56010, #18520, #50086, .T. ) ;
#64206=DIRECTION ( 'NONE',  ( 1.000000000000000000, 0.000000000000000000, 0.000000000000000000 ) ) ;
#64237=APPLICATION_CONTEXT ( 'automotive_design' ) ;
#64251=CARTESIAN_POINT ( 'NONE',  ( 6.938893903907228378E-15, 0.000000000000000000, 0.000000000000000000 ) ) ;
#64419=LINE ( 'NONE', #47852, #5730 ) ;
#64472=ORIENTED_EDGE ( 'NONE', *, *, #24284, .F. ) ;
#64538=LINE ( 'NONE', #46502, #68874 ) ;
#64716=VECTOR ( 'NONE', #37809, 1000.000000000000114 ) ;
#64731=( LENGTH_UNIT ( ) NAMED_UNIT ( * ) SI_UNIT ( .MILLI., .METRE. ) );
#64769=CARTESIAN_POINT ( 'NONE',  ( -42.50000000000000000, 1.932465207890948911E-15, 15.77977592589476608 ) ) ;
#64792=CARTESIAN_POINT ( 'NONE',  ( -11.70000000000000107, 2.535018874235021196E-15, 20.69999999999999929 ) ) ;
#64798=VECTOR ( 'NONE', #7393, 1000.000000000000000 ) ;
#64841=FACE_OUTER_BOUND ( 'NONE', #67012, .T. ) ;
#64878=DIRECTION ( 'NONE',  ( 0.000000000000000000, 0.000000000000000000, 1.000000000000000000 ) ) ;
#64955=ADVANCED_FACE ( 'NONE', ( #21081, #14712 ), #43679, .T. ) ;
#65025=AXIS2_PLACEMENT_3D ( 'NONE', #47638, #40902, #18684 ) ;
#65138=DIRECTION ( 'NONE',  ( 0.000000000000000000, 0.000000000000000000, -1.000000000000000000 ) ) ;
#65156=DIRECTION ( 'NONE',  ( 0.9781476007338070211, 0.000000000000000000, -0.2079116908177527367 ) ) ;
#65164=DIRECTION ( 'NONE',  ( 0.9781476007338070211, 0.000000000000000000, -0.2079116908177526257 ) ) ;
#65167=( LENGTH_UNIT ( ) NAMED_UNIT ( * ) SI_UNIT ( .MILLI., .METRE. ) );
#65283=CARTESIAN_POINT ( 'NONE',  ( -11.69999999999999929, 0.000000000000000000, -20.99999999999999645 ) ) ;
#65381=DIRECTION ( 'NONE',  ( 0.000000000000000000, -1.000000000000000000, 0.000000000000000000 ) ) ;
#65471=EDGE_CURVE ( 'NONE', #20976, #38823, #16488, .T. ) ;
#65507=DIRECTION ( 'NONE',  ( -0.000000000000000000, 0.000000000000000000, 1.000000000000000000 ) ) ;
#65546=EDGE_CURVE ( 'NONE', #3451, #16833, #26533, .T. ) ;
#65590=VERTEX_POINT ( 'NONE', #10471 ) ;
#65653=STYLED_ITEM ( 'NONE', ( #43297 ), #14123 ) ;
#65705=CARTESIAN_POINT ( 'NONE',  ( -12.00000000000000000, 0.000000000000000000, 0.000000000000000000 ) ) ;
#65838=ORIENTED_EDGE ( 'NONE', *, *, #13920, .T. ) ;
#65875=DIRECTION ( 'NONE',  ( 1.000000000000000000, 0.000000000000000000, 0.000000000000000000 ) ) ;
#65897=FACE_OUTER_BOUND ( 'NONE', #53914, .T. ) ;
#65931=VECTOR ( 'NONE', #8181, 1000.000000000000227 ) ;
#66054=VERTEX_POINT ( 'NONE', #70015 ) ;
#66124=CARTESIAN_POINT ( 'NONE',  ( -11.70000000000000107, 0.000000000000000000, -20.69999999999999929 ) ) ;
#66148=DIRECTION ( 'NONE',  ( -1.000000000000000000, -0.000000000000000000, -0.000000000000000000 ) ) ;
#66226=ORIENTED_EDGE ( 'NONE', *, *, #36266, .F. ) ;
#66449=DIRECTION ( 'NONE',  ( 0.000000000000000000, 0.000000000000000000, -1.000000000000000000 ) ) ;
#66509=EDGE_LOOP ( 'NONE', ( #28008, #55572 ) ) ;
#66597=LINE ( 'NONE', #26364, #8468 ) ;
#66620=DIRECTION ( 'NONE',  ( 1.000000000000000000, 0.000000000000000000, 0.000000000000000000 ) ) ;
#66683=FACE_OUTER_BOUND ( 'NONE', #42443, .T. ) ;
#66686=DIRECTION ( 'NONE',  ( 0.000000000000000000, 0.000000000000000000, -1.000000000000000000 ) ) ;
#66747=CARTESIAN_POINT ( 'NONE',  ( -3.000000000000002665, 2.353404862842836044E-15, 19.21700905503013601 ) ) ;
#67012=EDGE_LOOP ( 'NONE', ( #49812, #21758, #58820, #27130 ) ) ;
#67134=DIRECTION ( 'NONE',  ( 1.000000000000000000, 0.000000000000000000, 0.000000000000000000 ) ) ;
#67362=CARTESIAN_POINT ( 'NONE',  ( -12.00000000000000000, 0.000000000000000000, -17.30399999999999849 ) ) ;
#67380=AXIS2_PLACEMENT_3D ( 'NONE', #63415, #5908, #52115 ) ;
#67384=FACE_OUTER_BOUND ( 'NONE', #38675, .T. ) ;
#67475=AXIS2_PLACEMENT_3D ( 'NONE', #26667, #10124, #62396 ) ;
#67556=DIRECTION ( 'NONE',  ( 1.000000000000000000, 0.000000000000000000, 0.000000000000000000 ) ) ;
#67558=DIRECTION ( 'NONE',  ( 1.000000000000000000, 0.000000000000000000, 0.000000000000000000 ) ) ;
#67617=VERTEX_POINT ( 'NONE', #51736 ) ;
#67619=DIRECTION ( 'NONE',  ( -1.000000000000000000, 0.000000000000000000, 0.000000000000000000 ) ) ;
#67642=DIRECTION ( 'NONE',  ( 0.000000000000000000, 0.000000000000000000, -1.000000000000000000 ) ) ;
#67693=AXIS2_PLACEMENT_3D ( 'NONE', #63540, #63176, #782 ) ;
#67700=DIRECTION ( 'NONE',  ( 0.000000000000000000, 0.000000000000000000, -1.000000000000000000 ) ) ;
#67715=ORIENTED_EDGE ( 'NONE', *, *, #39727, .T. ) ;
#67775=ORIENTED_EDGE ( 'NONE', *, *, #13475, .F. ) ;
#67824=FACE_OUTER_BOUND ( 'NONE', #69608, .T. ) ;
#67860=CARTESIAN_POINT ( 'NONE',  ( -10.94538922500103162, 0.000000000000000000, 13.90444123027096879 ) ) ;
#67934=CIRCLE ( 'NONE', #23545, 20.64000000000000057 ) ;
#67990=DIRECTION ( 'NONE',  ( 0.000000000000000000, 0.000000000000000000, -1.000000000000000000 ) ) ;
#68090=DIRECTION ( 'NONE',  ( 1.000000000000000000, 0.000000000000000000, 0.000000000000000000 ) ) ;
#68149=VERTEX_POINT ( 'NONE', #9759 ) ;
#68198=DIRECTION ( 'NONE',  ( 0.000000000000000000, 0.000000000000000000, -1.000000000000000000 ) ) ;
#68300=VECTOR ( 'NONE', #30837, 1000.000000000000000 ) ;
#68339=VECTOR ( 'NONE', #10722, 1000.000000000000114 ) ;
#68638=FACE_OUTER_BOUND ( 'NONE', #56349, .T. ) ;
#68799=DIRECTION ( 'NONE',  ( 1.000000000000000000, 0.000000000000000000, 0.000000000000000000 ) ) ;
#68874=VECTOR ( 'NONE', #63440, 1000.000000000000114 ) ;
#68894=VERTEX_POINT ( 'NONE', #56274 ) ;
#68938=CARTESIAN_POINT ( 'NONE',  ( -42.50000000000000000, 1.702802944658382841E-15, 13.90444123027096879 ) ) ;
#69002=ORIENTED_EDGE ( 'NONE', *, *, #37205, .T. ) ;
#69017=DIRECTION ( 'NONE',  ( -0.7071067811865474617, 8.659560562354932858E-17, -0.7071067811865474617 ) ) ;
#69358=FACE_OUTER_BOUND ( 'NONE', #45120, .T. ) ;
#69389=VERTEX_POINT ( 'NONE', #73458 ) ;
#69408=VECTOR ( 'NONE', #29427, 1000.000000000000000 ) ;
#69439=DIRECTION ( 'NONE',  ( 1.000000000000000000, 0.000000000000000000, 0.000000000000000000 ) ) ;
#69495=EDGE_CURVE ( 'NONE', #24664, #66054, #64419, .T. ) ;
#69604=CYLINDRICAL_SURFACE ( 'NONE', #24714, 20.99999999999999645 ) ;
#69608=EDGE_LOOP ( 'NONE', ( #5376, #42072 ) ) ;
#69629=DIRECTION ( 'NONE',  ( 0.000000000000000000, 0.000000000000000000, 1.000000000000000000 ) ) ;
#69720=ORIENTED_EDGE ( 'NONE', *, *, #65546, .F. ) ;
#69751=CIRCLE ( 'NONE', #10935, 19.05560546998412974 ) ;
#69802=VERTEX_POINT ( 'NONE', #50442 ) ;
#69832=ADVANCED_FACE ( 'NONE', ( #29717 ), #40546, .T. ) ;
#69854=LINE ( 'NONE', #19093, #65931 ) ;
#69887=ORIENTED_EDGE ( 'NONE', *, *, #62590, .F. ) ;
#69956=CARTESIAN_POINT ( 'NONE',  ( -11.99999999999999645, 0.000000000000000000, 0.000000000000000000 ) ) ;
#69957=CARTESIAN_POINT ( 'NONE',  ( -3.000000000000002665, 0.000000000000000000, 0.000000000000000000 ) ) ;
#69961=DIRECTION ( 'NONE',  ( 0.000000000000000000, 0.000000000000000000, -1.000000000000000000 ) ) ;
#70015=CARTESIAN_POINT ( 'NONE',  ( -2.981742216678212820, 0.000000000000000000, -15.39727592608509177 ) ) ;
#70022=LINE ( 'NONE', #68938, #69408 ) ;
#70086=CYLINDRICAL_SURFACE ( 'NONE', #8362, 12.50000000000000000 ) ;
#70095=EDGE_CURVE ( 'NONE', #35854, #23517, #60181, .T. ) ;
#70315=DIRECTION ( 'NONE',  ( 1.000000000000000000, 0.000000000000000000, 0.000000000000000000 ) ) ;
#70336=ORIENTED_EDGE ( 'NONE', *, *, #43832, .F. ) ;
#70386=CARTESIAN_POINT ( 'NONE',  ( -2.977765906491215642, 0.000000000000000000, -15.39727592589476579 ) ) ;
#70427=DIRECTION ( 'NONE',  ( 0.000000000000000000, 0.000000000000000000, 1.000000000000000000 ) ) ;
#70462=( GEOMETRIC_REPRESENTATION_CONTEXT ( 3 ) GLOBAL_UNCERTAINTY_ASSIGNED_CONTEXT ( ( #51874 ) ) GLOBAL_UNIT_ASSIGNED_CONTEXT ( ( #64731, #1616, #41789 ) ) REPRESENTATION_CONTEXT ( 'NONE', 'WORKASPACE' ) );
#70478=DIRECTION ( 'NONE',  ( -1.000000000000000000, 0.000000000000000000, 0.000000000000000000 ) ) ;
#70491=EDGE_LOOP ( 'NONE', ( #17981, #51735 ) ) ;
#70527=ADVANCED_FACE ( 'NONE', ( #47410 ), #7051, .F. ) ;
#70566=AXIS2_PLACEMENT_3D ( 'NONE', #44146, #38131, #45272 ) ;
#70594=PLANE ( 'NONE',  #34828 ) ;
#70601=ADVANCED_FACE ( 'NONE', ( #35390 ), #40708, .F. ) ;
#70672=EDGE_CURVE ( 'NONE', #38741, #38823, #20307, .T. ) ;
#70926=DIRECTION ( 'NONE',  ( 0.000000000000000000, 0.000000000000000000, -1.000000000000000000 ) ) ;
#70965=AXIS2_PLACEMENT_3D ( 'NONE', #54588, #60248, #8727 ) ;
#71050=EDGE_CURVE ( 'NONE', #30425, #41023, #38340, .T. ) ;
#71060=CARTESIAN_POINT ( 'NONE',  ( -10.94538922500103162, 0.000000000000000000, 0.000000000000000000 ) ) ;
#71114=DIRECTION ( 'NONE',  ( -1.000000000000000000, -0.000000000000000000, -0.000000000000000000 ) ) ;
#71232=DIRECTION ( 'NONE',  ( 0.000000000000000000, 0.000000000000000000, 1.000000000000000000 ) ) ;
#71374=ORIENTED_EDGE ( 'NONE', *, *, #14696, .F. ) ;
#71484=DIRECTION ( 'NONE',  ( 0.000000000000000000, 0.000000000000000000, 1.000000000000000000 ) ) ;
#71516=( NAMED_UNIT ( * ) SI_UNIT ( $, .STERADIAN. ) SOLID_ANGLE_UNIT ( ) );
#71616=CARTESIAN_POINT ( 'NONE',  ( -10.94538922500103162, 1.915100337961297692E-15, -13.90444123027096879 ) ) ;
#71885=( LENGTH_UNIT ( ) NAMED_UNIT ( * ) SI_UNIT ( .MILLI., .METRE. ) );
#72054=VECTOR ( 'NONE', #17363, 1000.000000000000000 ) ;
#72139=ORIENTED_EDGE ( 'NONE', *, *, #62214, .F. ) ;
#72211=ORIENTED_EDGE ( 'NONE', *, *, #20877, .T. ) ;
#72215=ORIENTED_EDGE ( 'NONE', *, *, #18311, .F. ) ;
#72243=CARTESIAN_POINT ( 'NONE',  ( -11.63999999999999702, 0.000000000000000000, 12.50000000000000000 ) ) ;
#72275=DIRECTION ( 'NONE',  ( 0.000000000000000000, 0.000000000000000000, -1.000000000000000000 ) ) ;
#72280=ADVANCED_FACE ( 'NONE', ( #1458 ), #24078, .F. ) ;
#72402=FACE_OUTER_BOUND ( 'NONE', #73002, .T. ) ;
#72497=AXIS2_PLACEMENT_3D ( 'NONE', #51131, #50381, #4925 ) ;
#72733=ADVANCED_FACE ( 'NONE', ( #36916 ), #20344, .F. ) ;
#73002=EDGE_LOOP ( 'NONE', ( #19015, #3375, #41448, #18289 ) ) ;
#73147=VECTOR ( 'NONE', #21906, 1000.000000000000114 ) ;
#73347=ADVANCED_FACE ( 'NONE', ( #27401 ), #63628, .T. ) ;
#73458=CARTESIAN_POINT ( 'NONE',  ( -2.981742216678212820, 1.885622467846870828E-15, 15.39727592608509177 ) ) ;
#73496=CARTESIAN_POINT ( 'NONE',  ( -11.99999999999999645, 0.000000000000000000, 0.000000000000000000 ) ) ;
#73613=DIRECTION ( 'NONE',  ( 1.000000000000000000, 0.000000000000000000, 0.000000000000000000 ) ) ;
#73728=DIRECTION ( 'NONE',  ( 0.9781476007338069101, 0.000000000000000000, -0.2079116908177528755 ) ) ;
#73730=CIRCLE ( 'NONE', #72497, 12.85999999999999943 ) ;
#73745=ORIENTED_EDGE ( 'NONE', *, *, #35499, .F. ) ;
#73810=EDGE_LOOP ( 'NONE', ( #42305, #52595, #54540, #9874 ) ) ;
#73833=EDGE_CURVE ( 'NONE', #67617, #19812, #9723, .T. ) ;
#73981=LINE ( 'NONE', #22496, #47793 ) ;
#73994=VERTEX_POINT ( 'NONE', #287 ) ;
#74068=CARTESIAN_POINT ( 'NONE',  ( -11.63999999999999702, 0.000000000000000000, 0.000000000000000000 ) ) ;
#74248=CIRCLE ( 'NONE', #37018, 17.37152077436032371 ) ;
#74271=CARTESIAN_POINT ( 'NONE',  ( -11.68233973192911535, 0.000000000000000000, -17.37152077436032371 ) ) ;
ENDSEC;
END-ISO-10303-21;
